ISO-10303-21;
HEADER;
/* Generated by software containing ST-Developer
 * from STEP Tools, Inc. (www.steptools.com) 
 */

FILE_DESCRIPTION(
/* description */ ('PAT-054'),
/* implementation_level */ '2;1');

FILE_NAME(
/* name */ 'Flanged lead nut.step',
/* time_stamp */ '2026-10-29T16:38:13-07:00',
/* author */ (''),
/* organization */ (''),
/* preprocessor_version */ 'ST-DEVELOPER v20.2',
/* originating_system */ 'Autodesk Translation Framework v15.17.0.0',
/* authorisation */ '');

FILE_SCHEMA (('AUTOMOTIVE_DESIGN { 1 0 10303 214 3 1 1 }'));
ENDSEC;

DATA;
#10=MECHANICAL_DESIGN_GEOMETRIC_PRESENTATION_REPRESENTATION('',(#945),#33981);
#11=B_SPLINE_SURFACE_WITH_KNOTS('',3,3,((#22391,#22392,#22393,#22394,#22395,
#22396,#22397,#22398,#22399,#22400,#22401,#22402,#22403,#22404,#22405,#22406,
#22407,#22408,#22409,#22410,#22411,#22412,#22413,#22414,#22415,#22416,#22417,
#22418,#22419,#22420,#22421,#22422,#22423,#22424,#22425,#22426,#22427,#22428,
#22429,#22430,#22431,#22432,#22433,#22434,#22435,#22436,#22437,#22438,#22439,
#22440,#22441,#22442,#22443,#22444,#22445,#22446,#22447,#22448,#22449,#22450,
#22451,#22452,#22453,#22454,#22455,#22456,#22457,#22458,#22459,#22460,#22461,
#22462,#22463,#22464,#22465,#22466,#22467,#22468,#22469,#22470,#22471,#22472,
#22473,#22474,#22475,#22476,#22477,#22478,#22479,#22480,#22481,#22482,#22483,
#22484,#22485,#22486,#22487,#22488,#22489,#22490,#22491,#22492,#22493,#22494,
#22495,#22496,#22497,#22498,#22499,#22500,#22501,#22502,#22503,#22504,#22505),
(#22506,#22507,#22508,#22509,#22510,#22511,#22512,#22513,#22514,#22515,
#22516,#22517,#22518,#22519,#22520,#22521,#22522,#22523,#22524,#22525,#22526,
#22527,#22528,#22529,#22530,#22531,#22532,#22533,#22534,#22535,#22536,#22537,
#22538,#22539,#22540,#22541,#22542,#22543,#22544,#22545,#22546,#22547,#22548,
#22549,#22550,#22551,#22552,#22553,#22554,#22555,#22556,#22557,#22558,#22559,
#22560,#22561,#22562,#22563,#22564,#22565,#22566,#22567,#22568,#22569,#22570,
#22571,#22572,#22573,#22574,#22575,#22576,#22577,#22578,#22579,#22580,#22581,
#22582,#22583,#22584,#22585,#22586,#22587,#22588,#22589,#22590,#22591,#22592,
#22593,#22594,#22595,#22596,#22597,#22598,#22599,#22600,#22601,#22602,#22603,
#22604,#22605,#22606,#22607,#22608,#22609,#22610,#22611,#22612,#22613,#22614,
#22615,#22616,#22617,#22618,#22619,#22620),(#22621,#22622,#22623,#22624,
#22625,#22626,#22627,#22628,#22629,#22630,#22631,#22632,#22633,#22634,#22635,
#22636,#22637,#22638,#22639,#22640,#22641,#22642,#22643,#22644,#22645,#22646,
#22647,#22648,#22649,#22650,#22651,#22652,#22653,#22654,#22655,#22656,#22657,
#22658,#22659,#22660,#22661,#22662,#22663,#22664,#22665,#22666,#22667,#22668,
#22669,#22670,#22671,#22672,#22673,#22674,#22675,#22676,#22677,#22678,#22679,
#22680,#22681,#22682,#22683,#22684,#22685,#22686,#22687,#22688,#22689,#22690,
#22691,#22692,#22693,#22694,#22695,#22696,#22697,#22698,#22699,#22700,#22701,
#22702,#22703,#22704,#22705,#22706,#22707,#22708,#22709,#22710,#22711,#22712,
#22713,#22714,#22715,#22716,#22717,#22718,#22719,#22720,#22721,#22722,#22723,
#22724,#22725,#22726,#22727,#22728,#22729,#22730,#22731,#22732,#22733,#22734,
#22735),(#22736,#22737,#22738,#22739,#22740,#22741,#22742,#22743,#22744,
#22745,#22746,#22747,#22748,#22749,#22750,#22751,#22752,#22753,#22754,#22755,
#22756,#22757,#22758,#22759,#22760,#22761,#22762,#22763,#22764,#22765,#22766,
#22767,#22768,#22769,#22770,#22771,#22772,#22773,#22774,#22775,#22776,#22777,
#22778,#22779,#22780,#22781,#22782,#22783,#22784,#22785,#22786,#22787,#22788,
#22789,#22790,#22791,#22792,#22793,#22794,#22795,#22796,#22797,#22798,#22799,
#22800,#22801,#22802,#22803,#22804,#22805,#22806,#22807,#22808,#22809,#22810,
#22811,#22812,#22813,#22814,#22815,#22816,#22817,#22818,#22819,#22820,#22821,
#22822,#22823,#22824,#22825,#22826,#22827,#22828,#22829,#22830,#22831,#22832,
#22833,#22834,#22835,#22836,#22837,#22838,#22839,#22840,#22841,#22842,#22843,
#22844,#22845,#22846,#22847,#22848,#22849,#22850)),.UNSPECIFIED.,.F.,.F.,
 .F.,(4,4),(4,1,1,1,1,1,1,1,1,1,1,1,1,1,1,1,1,1,1,1,1,1,1,1,1,1,1,1,1,1,
1,1,1,1,1,1,1,1,1,1,1,1,1,1,1,1,1,1,1,1,1,1,1,1,1,1,1,1,1,1,1,1,1,1,1,1,
1,1,1,1,1,1,1,1,1,1,1,1,1,1,1,1,1,1,1,1,1,1,1,1,1,1,1,1,1,1,1,1,1,1,1,1,
1,1,1,1,1,1,1,1,1,1,4),(0.,0.173020531651036),(12.1475814751569,12.6421543672732,
13.1367272593894,13.6313001515056,14.1258730436219,14.6204459357381,15.1150188278544,
15.6095917199706,16.1041646120869,16.5987375042031,17.0933103963194,17.5878832884356,
18.0824561805519,18.5770290726681,19.0716019647843,19.5661748569006,20.0607477490168,
20.5553206411331,21.0498935332493,21.5444664253656,22.0390393174818,22.5336122095981,
23.0281851017143,23.5227579938306,24.0173308859468,24.511903778063,25.0064766701793,
25.5010495622955,25.9956224544118,26.490195346528,26.9847682386443,27.4793411307605,
27.9739140228768,28.468486914993,28.9630598071093,29.4576326992255,29.9522055913417,
30.446778483458,30.9413513755742,31.4359242676905,31.9304971598067,32.425070051923,
32.9196429440392,33.4142158361555,33.9087887282717,34.403361620388,34.8979345125042,
35.3925074046204,35.8870802967367,36.3816531888529,36.8762260809692,37.3707989730854,
37.8653718652017,38.3599447573179,38.8545176494342,39.3490905415504,39.8436634336667,
40.3382363257829,40.8328092178991,41.3273821100154,41.8219550021316,42.3165278942479,
42.8111007863641,43.3056736784804,43.8002465705966,44.2948194627129,44.7893923548291,
45.2839652469454,45.7785381390616,46.2731110311778,46.7676839232941,47.2622568154103,
47.7568297075266,48.2514025996428,48.7459754917591,49.2405483838753,49.7351212759916,
50.2296941681078,50.7242670602241,51.2188399523403,51.7134128444565,52.2079857365728,
52.702558628689,53.1971315208053,53.6917044129215,54.1862773050378,54.680850197154,
55.1754230892703,55.6699959813865,56.1645688735028,56.659141765619,57.1537146577353,
57.6482875498515,58.1428604419677,58.637433334084,59.1320062262002,59.6265791183165,
60.1211520104327,60.615724902549,61.1102977946652,61.6048706867815,62.0994435788977,
62.5940164710139,63.0885893631302,63.5831622552464,64.0777351473627,64.5723080394789,
65.0668809315952,65.5614538237114,66.0560267158277,66.5505996079439,67.0451725000601,
67.5397453921764),.UNSPECIFIED.);
#12=B_SPLINE_SURFACE_WITH_KNOTS('',3,3,((#22950,#22951,#22952,#22953,#22954,
#22955,#22956,#22957,#22958,#22959,#22960,#22961,#22962,#22963,#22964,#22965,
#22966,#22967,#22968,#22969,#22970,#22971,#22972,#22973,#22974,#22975,#22976,
#22977,#22978,#22979,#22980,#22981,#22982,#22983,#22984,#22985,#22986,#22987,
#22988,#22989,#22990,#22991,#22992,#22993,#22994,#22995,#22996,#22997,#22998,
#22999,#23000,#23001,#23002,#23003,#23004,#23005,#23006,#23007,#23008,#23009,
#23010,#23011,#23012,#23013,#23014,#23015,#23016,#23017,#23018,#23019,#23020,
#23021,#23022,#23023,#23024,#23025,#23026,#23027,#23028,#23029,#23030,#23031,
#23032,#23033,#23034,#23035,#23036,#23037,#23038,#23039,#23040,#23041,#23042,
#23043,#23044,#23045,#23046,#23047,#23048,#23049,#23050,#23051,#23052,#23053,
#23054,#23055,#23056,#23057,#23058,#23059,#23060,#23061,#23062,#23063,#23064),
(#23065,#23066,#23067,#23068,#23069,#23070,#23071,#23072,#23073,#23074,
#23075,#23076,#23077,#23078,#23079,#23080,#23081,#23082,#23083,#23084,#23085,
#23086,#23087,#23088,#23089,#23090,#23091,#23092,#23093,#23094,#23095,#23096,
#23097,#23098,#23099,#23100,#23101,#23102,#23103,#23104,#23105,#23106,#23107,
#23108,#23109,#23110,#23111,#23112,#23113,#23114,#23115,#23116,#23117,#23118,
#23119,#23120,#23121,#23122,#23123,#23124,#23125,#23126,#23127,#23128,#23129,
#23130,#23131,#23132,#23133,#23134,#23135,#23136,#23137,#23138,#23139,#23140,
#23141,#23142,#23143,#23144,#23145,#23146,#23147,#23148,#23149,#23150,#23151,
#23152,#23153,#23154,#23155,#23156,#23157,#23158,#23159,#23160,#23161,#23162,
#23163,#23164,#23165,#23166,#23167,#23168,#23169,#23170,#23171,#23172,#23173,
#23174,#23175,#23176,#23177,#23178,#23179),(#23180,#23181,#23182,#23183,
#23184,#23185,#23186,#23187,#23188,#23189,#23190,#23191,#23192,#23193,#23194,
#23195,#23196,#23197,#23198,#23199,#23200,#23201,#23202,#23203,#23204,#23205,
#23206,#23207,#23208,#23209,#23210,#23211,#23212,#23213,#23214,#23215,#23216,
#23217,#23218,#23219,#23220,#23221,#23222,#23223,#23224,#23225,#23226,#23227,
#23228,#23229,#23230,#23231,#23232,#23233,#23234,#23235,#23236,#23237,#23238,
#23239,#23240,#23241,#23242,#23243,#23244,#23245,#23246,#23247,#23248,#23249,
#23250,#23251,#23252,#23253,#23254,#23255,#23256,#23257,#23258,#23259,#23260,
#23261,#23262,#23263,#23264,#23265,#23266,#23267,#23268,#23269,#23270,#23271,
#23272,#23273,#23274,#23275,#23276,#23277,#23278,#23279,#23280,#23281,#23282,
#23283,#23284,#23285,#23286,#23287,#23288,#23289,#23290,#23291,#23292,#23293,
#23294),(#23295,#23296,#23297,#23298,#23299,#23300,#23301,#23302,#23303,
#23304,#23305,#23306,#23307,#23308,#23309,#23310,#23311,#23312,#23313,#23314,
#23315,#23316,#23317,#23318,#23319,#23320,#23321,#23322,#23323,#23324,#23325,
#23326,#23327,#23328,#23329,#23330,#23331,#23332,#23333,#23334,#23335,#23336,
#23337,#23338,#23339,#23340,#23341,#23342,#23343,#23344,#23345,#23346,#23347,
#23348,#23349,#23350,#23351,#23352,#23353,#23354,#23355,#23356,#23357,#23358,
#23359,#23360,#23361,#23362,#23363,#23364,#23365,#23366,#23367,#23368,#23369,
#23370,#23371,#23372,#23373,#23374,#23375,#23376,#23377,#23378,#23379,#23380,
#23381,#23382,#23383,#23384,#23385,#23386,#23387,#23388,#23389,#23390,#23391,
#23392,#23393,#23394,#23395,#23396,#23397,#23398,#23399,#23400,#23401,#23402,
#23403,#23404,#23405,#23406,#23407,#23408,#23409)),.UNSPECIFIED.,.F.,.F.,
 .F.,(4,4),(4,1,1,1,1,1,1,1,1,1,1,1,1,1,1,1,1,1,1,1,1,1,1,1,1,1,1,1,1,1,
1,1,1,1,1,1,1,1,1,1,1,1,1,1,1,1,1,1,1,1,1,1,1,1,1,1,1,1,1,1,1,1,1,1,1,1,
1,1,1,1,1,1,1,1,1,1,1,1,1,1,1,1,1,1,1,1,1,1,1,1,1,1,1,1,1,1,1,1,1,1,1,1,
1,1,1,1,1,1,1,1,1,1,4),(0.,0.173020531651036),(15.1888611523549,15.6834340444711,
16.1780069365874,16.6725798287036,17.1671527208199,17.6617256129361,18.1562985050523,
18.6508713971686,19.1454442892848,19.6400171814011,20.1345900735173,20.6291629656336,
21.1237358577498,21.6183087498661,22.1128816419823,22.6074545340986,23.1020274262148,
23.596600318331,24.0911732104473,24.5857461025635,25.0803189946798,25.574891886796,
26.0694647789123,26.5640376710285,27.0586105631448,27.553183455261,28.0477563473773,
28.5423292394935,29.0369021316097,29.531475023726,30.0260479158422,30.5206208079585,
31.0151937000747,31.509766592191,32.0043394843072,32.4989123764235,32.9934852685397,
33.488058160656,33.9826310527722,34.4772039448884,34.9717768370047,35.4663497291209,
35.9609226212372,36.4554955133534,36.9500684054697,37.4446412975859,37.9392141897022,
38.4337870818184,38.9283599739347,39.4229328660509,39.9175057581671,40.4120786502834,
40.9066515423996,41.4012244345159,41.8957973266321,42.3903702187484,42.8849431108646,
43.3795160029809,43.8740888950971,44.3686617872134,44.8632346793296,45.3578075714458,
45.8523804635621,46.3469533556783,46.8415262477946,47.3360991399108,47.8306720320271,
48.3252449241433,48.8198178162596,49.3143907083758,49.8089636004921,50.3035364926083,
50.7981093847245,51.2926822768408,51.787255168957,52.2818280610733,52.7764009531895,
53.2709738453058,53.765546737422,54.2601196295383,54.7546925216545,55.2492654137708,
55.743838305887,56.2384111980032,56.7329840901195,57.2275569822357,57.722129874352,
58.2167027664682,58.7112756585845,59.2058485507007,59.700421442817,60.1949943349332,
60.6895672270495,61.1841401191657,61.6787130112819,62.1732859033982,62.6678587955144,
63.1624316876307,63.6570045797469,64.1515774718632,64.6461503639794,65.1407232560957,
65.6352961482119,66.1298690403281,66.6244419324444,67.1190148245607,67.6135877166769,
68.1081606087931,68.6027335009094,69.0973063930256,69.5918792851419,70.0864521772581,
70.5810250693744),.UNSPECIFIED.);
#435=B_SPLINE_CURVE_WITH_KNOTS('',3,(#21347,#21348,#21349,#21350,#21351,
#21352,#21353,#21354,#21355,#21356,#21357,#21358,#21359,#21360,#21361,#21362,
#21363,#21364,#21365,#21366,#21367,#21368,#21369,#21370,#21371),
 .UNSPECIFIED.,.F.,.F.,(4,3,3,3,3,3,3,3,4),(-3.56038179279204,-3.46201024481372,
-2.96743735269747,-2.47286446058123,-1.97829156846498,-1.48371867634874,
-0.989145784232491,-0.494572892116246,0.),.UNSPECIFIED.);
#436=B_SPLINE_CURVE_WITH_KNOTS('',3,(#21374,#21375,#21376,#21377,#21378,
#21379,#21380,#21381,#21382,#21383,#21384,#21385,#21386,#21387,#21388,#21389,
#21390,#21391,#21392,#21393,#21394,#21395,#21396,#21397,#21398,#21399,#21400,
#21401,#21402,#21403,#21404,#21405,#21406,#21407,#21408,#21409,#21410,#21411,
#21412,#21413),.UNSPECIFIED.,.F.,.F.,(4,3,3,3,3,3,3,3,3,3,3,3,3,4),(0.937891254796418,
0.989145784232494,1.48371867634874,1.97829156846498,2.47286446058123,2.96743735269748,
3.46201024481372,3.95658313692997,4.45115602904621,4.94572892116246,5.44030181327871,
5.93487470539495,6.42944759751119,6.80228742277363),.UNSPECIFIED.);
#437=B_SPLINE_CURVE_WITH_KNOTS('',3,(#21418,#21419,#21420,#21421,#21422,
#21423,#21424,#21425,#21426,#21427,#21428,#21429,#21430,#21431,#21432,#21433,
#21434,#21435,#21436,#21437,#21438,#21439,#21440,#21441,#21442,#21443,#21444,
#21445,#21446,#21447,#21448,#21449,#21450,#21451,#21452,#21453,#21454,#21455,
#21456,#21457),.UNSPECIFIED.,.F.,.F.,(4,3,3,3,3,3,3,3,3,3,3,3,3,4),(-9.8435670999716,
-9.39688495020867,-8.90231205809242,-8.40773916597618,-7.91316627385993,
-7.41859338174369,-6.92402048962744,-6.42944759751119,-5.93487470539495,
-5.4403018132787,-4.94572892116246,-4.45115602904621,-3.95658313692996,
-3.56038179279204),.UNSPECIFIED.);
#438=B_SPLINE_CURVE_WITH_KNOTS('',3,(#21458,#21459,#21460,#21461,#21462,
#21463,#21464,#21465,#21466,#21467,#21468,#21469,#21470,#21471,#21472,#21473,
#21474,#21475,#21476,#21477,#21478,#21479,#21480,#21481,#21482,#21483,#21484,
#21485,#21486,#21487,#21488,#21489,#21490,#21491,#21492,#21493,#21494,#21495,
#21496,#21497,#21498,#21499,#21500),.UNSPECIFIED.,.F.,.F.,(4,3,3,3,3,3,
3,3,3,3,3,3,3,3,4),(6.80228742277363,6.92402048962744,7.41859338174369,
7.91316627385993,8.40773916597617,8.90231205809242,9.39688495020867,9.89145784232491,
10.3860307344412,10.8806036265574,11.3751765186736,11.8697494107899,12.3643223029061,
12.8588951950224,13.0854727299532),.UNSPECIFIED.);
#439=B_SPLINE_CURVE_WITH_KNOTS('',3,(#21505,#21506,#21507,#21508,#21509,
#21510,#21511,#21512,#21513,#21514,#21515,#21516,#21517,#21518,#21519,#21520,
#21521,#21522,#21523,#21524,#21525,#21526,#21527,#21528,#21529,#21530,#21531,
#21532,#21533,#21534,#21535,#21536,#21537,#21538,#21539,#21540,#21541,#21542,
#21543,#21544,#21545,#21546,#21547),.UNSPECIFIED.,.F.,.F.,(4,3,3,3,3,3,
3,3,3,3,3,3,3,3,4),(-16.1267524071512,-15.8263325477199,-15.3317596556036,
-14.8371867634874,-14.3426138713711,-13.8480409792549,-13.3534680871386,
-12.8588951950224,-12.3643223029061,-11.8697494107899,-11.3751765186736,
-10.8806036265574,-10.3860307344412,-9.89145784232491,-9.8435670999716),
 .UNSPECIFIED.);
#440=B_SPLINE_CURVE_WITH_KNOTS('',3,(#21548,#21549,#21550,#21551,#21552,
#21553,#21554,#21555,#21556,#21557,#21558,#21559,#21560,#21561,#21562,#21563,
#21564,#21565,#21566,#21567,#21568,#21569,#21570,#21571,#21572,#21573,#21574,
#21575,#21576,#21577,#21578,#21579,#21580,#21581,#21582,#21583,#21584,#21585,
#21586,#21587,#21588,#21589,#21590),.UNSPECIFIED.,.F.,.F.,(4,3,3,3,3,3,
3,3,3,3,3,3,3,3,4),(13.0854727299532,13.3534680871386,13.8480409792549,
14.3426138713711,14.8371867634874,15.3317596556036,15.8263325477199,16.3209054398361,
16.8154783319523,17.3100512240686,17.8046241161848,18.2991970083011,18.7937699004173,
19.2883427925336,19.3686580371328),.UNSPECIFIED.);
#441=B_SPLINE_CURVE_WITH_KNOTS('',3,(#21595,#21596,#21597,#21598,#21599,
#21600,#21601,#21602,#21603,#21604,#21605,#21606,#21607,#21608,#21609,#21610,
#21611,#21612,#21613,#21614,#21615,#21616,#21617,#21618,#21619,#21620,#21621,
#21622,#21623,#21624,#21625,#21626,#21627,#21628,#21629,#21630,#21631,#21632,
#21633,#21634,#21635,#21636,#21637),.UNSPECIFIED.,.F.,.F.,(4,3,3,3,3,3,
3,3,3,3,3,3,3,3,4),(-22.4099377143308,-22.2557801452311,-21.7612072531148,
-21.2666343609986,-20.7720614688823,-20.2774885767661,-19.7829156846498,
-19.2883427925336,-18.7937699004173,-18.2991970083011,-17.8046241161848,
-17.3100512240686,-16.8154783319523,-16.3209054398361,-16.1267524071512),
 .UNSPECIFIED.);
#442=B_SPLINE_CURVE_WITH_KNOTS('',3,(#21638,#21639,#21640,#21641,#21642,
#21643,#21644,#21645,#21646,#21647,#21648,#21649,#21650,#21651,#21652,#21653,
#21654,#21655,#21656,#21657,#21658,#21659,#21660,#21661,#21662,#21663,#21664,
#21665,#21666,#21667,#21668,#21669,#21670,#21671,#21672,#21673,#21674,#21675,
#21676,#21677),.UNSPECIFIED.,.F.,.F.,(4,3,3,3,3,3,3,3,3,3,3,3,3,4),(19.3686580371328,
19.7829156846498,20.2774885767661,20.7720614688823,21.2666343609986,21.7612072531148,
22.255780145231,22.7503530373473,23.2449259294635,23.7394988215798,24.234071713696,
24.7286446058123,25.2232174979285,25.6518433443124),.UNSPECIFIED.);
#443=B_SPLINE_CURVE_WITH_KNOTS('',3,(#21682,#21683,#21684,#21685,#21686,
#21687,#21688,#21689,#21690,#21691,#21692,#21693,#21694,#21695,#21696,#21697,
#21698,#21699,#21700,#21701,#21702,#21703,#21704,#21705,#21706,#21707,#21708,
#21709,#21710,#21711,#21712,#21713,#21714,#21715,#21716,#21717,#21718,#21719,
#21720,#21721,#21722,#21723,#21724),.UNSPECIFIED.,.F.,.F.,(4,3,3,3,3,3,
3,3,3,3,3,3,3,3,4),(-28.6931230215104,-28.6852277427422,-28.190654850626,
-27.6960819585097,-27.2015090663935,-26.7069361742773,-26.212363282161,
-25.7177903900448,-25.2232174979285,-24.7286446058123,-24.234071713696,
-23.7394988215798,-23.2449259294635,-22.7503530373473,-22.4099377143308),
 .UNSPECIFIED.);
#444=B_SPLINE_CURVE_WITH_KNOTS('',3,(#21725,#21726,#21727,#21728,#21729,
#21730,#21731,#21732,#21733,#21734,#21735,#21736,#21737,#21738,#21739,#21740,
#21741,#21742,#21743,#21744,#21745,#21746,#21747,#21748,#21749,#21750,#21751,
#21752,#21753,#21754,#21755,#21756,#21757,#21758,#21759,#21760,#21761,#21762,
#21763,#21764,#21765,#21766,#21767),.UNSPECIFIED.,.F.,.F.,(4,3,3,3,3,3,
3,3,3,3,3,3,3,3,4),(25.6518433443124,25.7177903900448,26.212363282161,26.7069361742773,
27.2015090663935,27.6960819585097,28.190654850626,28.6852277427422,29.1798006348585,
29.6743735269747,30.168946419091,30.6635193112072,31.1580922033235,31.6526650954397,
31.935028651492),.UNSPECIFIED.);
#445=B_SPLINE_CURVE_WITH_KNOTS('',3,(#21772,#21773,#21774,#21775,#21776,
#21777,#21778,#21779,#21780,#21781,#21782,#21783,#21784,#21785,#21786,#21787,
#21788,#21789,#21790,#21791,#21792,#21793,#21794,#21795,#21796,#21797,#21798,
#21799,#21800,#21801,#21802,#21803,#21804,#21805,#21806,#21807,#21808,#21809,
#21810,#21811),.UNSPECIFIED.,.F.,.F.,(4,3,3,3,3,3,3,3,3,3,3,3,3,4),(-34.97630832869,
-34.6201024481372,-34.1255295560209,-33.6309566639047,-33.1363837717884,
-32.6418108796722,-32.147237987556,-31.6526650954397,-31.1580922033235,
-30.6635193112072,-30.168946419091,-29.6743735269747,-29.1798006348585,
-28.6931230215104),.UNSPECIFIED.);
#446=B_SPLINE_CURVE_WITH_KNOTS('',3,(#21812,#21813,#21814,#21815,#21816,
#21817,#21818,#21819,#21820,#21821,#21822,#21823,#21824,#21825,#21826,#21827,
#21828,#21829,#21830,#21831,#21832,#21833,#21834,#21835,#21836,#21837,#21838,
#21839,#21840,#21841,#21842,#21843,#21844,#21845,#21846,#21847,#21848,#21849,
#21850,#21851,#21852,#21853,#21854),.UNSPECIFIED.,.F.,.F.,(4,3,3,3,3,3,
3,3,3,3,3,3,3,3,4),(31.935028651492,32.147237987556,32.6418108796722,33.1363837717885,
33.6309566639047,34.1255295560209,34.6201024481372,35.1146753402534,35.6092482323697,
36.1038211244859,36.5983940166022,37.0929669087184,37.5875398008347,38.0821126929509,
38.2182139586716),.UNSPECIFIED.);
#447=B_SPLINE_CURVE_WITH_KNOTS('',3,(#21859,#21860,#21861,#21862,#21863,
#21864,#21865,#21866,#21867,#21868,#21869,#21870,#21871,#21872,#21873,#21874,
#21875,#21876,#21877,#21878,#21879,#21880,#21881,#21882,#21883,#21884,#21885,
#21886,#21887,#21888,#21889,#21890,#21891,#21892,#21893,#21894,#21895,#21896,
#21897,#21898,#21899,#21900,#21901),.UNSPECIFIED.,.F.,.F.,(4,3,3,3,3,3,
3,3,3,3,3,3,3,3,4),(-41.2594936358696,-41.0495500456484,-40.5549771535321,
-40.0604042614159,-39.5658313692996,-39.0712584771834,-38.5766855850671,
-38.0821126929509,-37.5875398008347,-37.0929669087184,-36.5983940166022,
-36.1038211244859,-35.6092482323697,-35.1146753402534,-34.97630832869),
 .UNSPECIFIED.);
#448=B_SPLINE_CURVE_WITH_KNOTS('',3,(#21902,#21903,#21904,#21905,#21906,
#21907,#21908,#21909,#21910,#21911,#21912,#21913,#21914,#21915,#21916,#21917,
#21918,#21919,#21920,#21921,#21922,#21923,#21924,#21925,#21926,#21927,#21928,
#21929,#21930,#21931,#21932,#21933,#21934,#21935,#21936,#21937,#21938,#21939,
#21940,#21941),.UNSPECIFIED.,.F.,.F.,(4,3,3,3,3,3,3,3,3,3,3,3,3,4),(38.2182139586716,
38.5766855850671,39.0712584771834,39.5658313692996,40.0604042614159,40.5549771535321,
41.0495500456484,41.5441229377646,42.0386958298809,42.5332687219971,43.0278416141134,
43.5224145062296,44.0169873983459,44.5013992658512),.UNSPECIFIED.);
#449=B_SPLINE_CURVE_WITH_KNOTS('',3,(#21946,#21947,#21948,#21949,#21950,
#21951,#21952,#21953,#21954,#21955,#21956,#21957,#21958,#21959,#21960,#21961,
#21962,#21963,#21964,#21965,#21966,#21967,#21968,#21969,#21970,#21971,#21972,
#21973,#21974,#21975,#21976,#21977,#21978,#21979,#21980,#21981,#21982,#21983,
#21984,#21985,#21986,#21987,#21988),.UNSPECIFIED.,.F.,.F.,(4,3,3,3,3,3,
3,3,3,3,3,3,3,3,4),(-47.5426789430491,-47.4789976431596,-46.9844247510433,
-46.4898518589271,-45.9952789668108,-45.5007060746946,-45.0061331825783,
-44.5115602904621,-44.0169873983458,-43.5224145062296,-43.0278416141134,
-42.5332687219971,-42.0386958298809,-41.5441229377646,-41.2594936358696),
 .UNSPECIFIED.);
#450=B_SPLINE_CURVE_WITH_KNOTS('',3,(#21989,#21990,#21991,#21992,#21993,
#21994,#21995,#21996,#21997,#21998,#21999,#22000,#22001,#22002,#22003,#22004,
#22005,#22006,#22007,#22008,#22009,#22010,#22011,#22012,#22013,#22014,#22015,
#22016,#22017,#22018,#22019,#22020,#22021,#22022,#22023,#22024,#22025,#22026,
#22027,#22028,#22029,#22030,#22031),.UNSPECIFIED.,.F.,.F.,(4,3,3,3,3,3,
3,3,3,3,3,3,3,3,4),(44.5013992658512,44.5115602904621,45.0061331825783,
45.5007060746946,45.9952789668108,46.4898518589271,46.9844247510433,47.4789976431596,
47.9735705352758,48.4681434273921,48.9627163195083,49.4572892116245,49.9518621037408,
50.446434995857,50.7845845730308),.UNSPECIFIED.);
#451=B_SPLINE_CURVE_WITH_KNOTS('',3,(#22038,#22039,#22040,#22041,#22042,
#22043,#22044,#22045,#22046,#22047),.UNSPECIFIED.,.F.,.F.,(4,3,3,4),(-54.4542726622231,
-54.403018132787,-53.9084452406708,-53.8258642502287),.UNSPECIFIED.);
#452=B_SPLINE_CURVE_WITH_KNOTS('',3,(#22053,#22054,#22055,#22056,#22057,
#22058,#22059),.UNSPECIFIED.,.F.,.F.,(4,1,1,1,4),(65.9734457253856,66.0560267158277,
66.5505996079439,67.0451725000601,67.5397453921764),.UNSPECIFIED.);
#453=B_SPLINE_CURVE_WITH_KNOTS('',3,(#22062,#22063,#22064,#22065,#22066,
#22067,#22068,#22069,#22070,#22071,#22072,#22073),.UNSPECIFIED.,.F.,.F.,
(4,1,1,1,1,1,1,1,1,4),(65.9734457253856,66.1298690403281,66.6244419324444,
67.1190148245607,67.6135877166769,68.1081606087931,68.6027335009094,69.0973063930256,
69.5918792851419,69.643133814578),.UNSPECIFIED.);
#454=B_SPLINE_CURVE_WITH_KNOTS('',3,(#22078,#22079,#22080,#22081,#22082,
#22083,#22084,#22085,#22086,#22087,#22088,#22089,#22090,#22091,#22092,#22093),
 .UNSPECIFIED.,.F.,.F.,(4,1,1,1,1,1,1,1,1,1,1,1,1,4),(59.6902604182061,
60.1211520104327,60.615724902549,61.1102977946652,61.6048706867815,62.0994435788977,
62.5940164710139,63.0885893631302,63.5831622552464,64.0777351473627,64.5723080394789,
65.0668809315952,65.5614538237114,65.9734457253856),.UNSPECIFIED.);
#455=B_SPLINE_CURVE_WITH_KNOTS('',3,(#22094,#22095,#22096,#22097,#22098,
#22099,#22100,#22101,#22102,#22103,#22104,#22105,#22106,#22107,#22108,#22109,
#22110),.UNSPECIFIED.,.F.,.F.,(4,1,1,1,1,1,1,1,1,1,1,1,1,1,4),(59.6902604182061,
59.700421442817,60.1949943349332,60.6895672270495,61.1841401191657,61.6787130112819,
62.1732859033982,62.6678587955144,63.1624316876307,63.6570045797469,64.1515774718632,
64.6461503639794,65.1407232560957,65.6352961482119,65.9734457253856),
 .UNSPECIFIED.);
#456=B_SPLINE_CURVE_WITH_KNOTS('',3,(#22115,#22116,#22117,#22118,#22119,
#22120,#22121,#22122,#22123,#22124,#22125,#22126,#22127,#22128,#22129,#22130,
#22131),.UNSPECIFIED.,.F.,.F.,(4,1,1,1,1,1,1,1,1,1,1,1,1,1,4),(53.4070751110264,
53.6917044129215,54.1862773050378,54.680850197154,55.1754230892703,55.6699959813865,
56.1645688735028,56.659141765619,57.1537146577353,57.6482875498515,58.1428604419677,
58.637433334084,59.1320062262002,59.6265791183165,59.6902604182061),
 .UNSPECIFIED.);
#457=B_SPLINE_CURVE_WITH_KNOTS('',3,(#22132,#22133,#22134,#22135,#22136,
#22137,#22138,#22139,#22140,#22141,#22142,#22143,#22144,#22145,#22146,#22147),
 .UNSPECIFIED.,.F.,.F.,(4,1,1,1,1,1,1,1,1,1,1,1,1,4),(53.4070751110264,
53.765546737422,54.2601196295383,54.7546925216545,55.2492654137708,55.743838305887,
56.2384111980032,56.7329840901195,57.2275569822357,57.722129874352,58.2167027664682,
58.7112756585845,59.2058485507007,59.6902604182061),.UNSPECIFIED.);
#458=B_SPLINE_CURVE_WITH_KNOTS('',3,(#22152,#22153,#22154,#22155,#22156,
#22157,#22158,#22159,#22160,#22161,#22162,#22163,#22164,#22165,#22166,#22167,
#22168),.UNSPECIFIED.,.F.,.F.,(4,1,1,1,1,1,1,1,1,1,1,1,1,1,4),(47.1238898038469,
47.2622568154103,47.7568297075266,48.2514025996428,48.7459754917591,49.2405483838753,
49.7351212759916,50.2296941681078,50.7242670602241,51.2188399523403,51.7134128444565,
52.2079857365728,52.702558628689,53.1971315208053,53.4070751110264),
 .UNSPECIFIED.);
#459=B_SPLINE_CURVE_WITH_KNOTS('',3,(#22169,#22170,#22171,#22172,#22173,
#22174,#22175,#22176,#22177,#22178,#22179,#22180,#22181,#22182,#22183,#22184,
#22185),.UNSPECIFIED.,.F.,.F.,(4,1,1,1,1,1,1,1,1,1,1,1,1,1,4),(47.1238898038469,
47.3360991399108,47.8306720320271,48.3252449241433,48.8198178162596,49.3143907083758,
49.8089636004921,50.3035364926083,50.7981093847245,51.2926822768408,51.787255168957,
52.2818280610733,52.7764009531895,53.2709738453058,53.4070751110264),
 .UNSPECIFIED.);
#460=B_SPLINE_CURVE_WITH_KNOTS('',3,(#22190,#22191,#22192,#22193,#22194,
#22195,#22196,#22197,#22198,#22199,#22200,#22201,#22202,#22203,#22204,#22205),
 .UNSPECIFIED.,.F.,.F.,(4,1,1,1,1,1,1,1,1,1,1,1,1,4),(40.8407044966673,
41.3273821100154,41.8219550021316,42.3165278942479,42.8111007863641,43.3056736784804,
43.8002465705966,44.2948194627129,44.7893923548291,45.2839652469454,45.7785381390616,
46.2731110311778,46.7676839232941,47.1238898038469),.UNSPECIFIED.);
#461=B_SPLINE_CURVE_WITH_KNOTS('',3,(#22206,#22207,#22208,#22209,#22210,
#22211,#22212,#22213,#22214,#22215,#22216,#22217,#22218,#22219,#22220,#22221,
#22222),.UNSPECIFIED.,.F.,.F.,(4,1,1,1,1,1,1,1,1,1,1,1,1,1,4),(40.8407044966673,
40.9066515423996,41.4012244345159,41.8957973266321,42.3903702187484,42.8849431108646,
43.3795160029809,43.8740888950971,44.3686617872134,44.8632346793296,45.3578075714458,
45.8523804635621,46.3469533556783,46.8415262477946,47.1238898038469),
 .UNSPECIFIED.);
#462=B_SPLINE_CURVE_WITH_KNOTS('',3,(#22227,#22228,#22229,#22230,#22231,
#22232,#22233,#22234,#22235,#22236,#22237,#22238,#22239,#22240,#22241,#22242,
#22243),.UNSPECIFIED.,.F.,.F.,(4,1,1,1,1,1,1,1,1,1,1,1,1,1,4),(34.5575191894877,
34.8979345125042,35.3925074046204,35.8870802967367,36.3816531888529,36.8762260809692,
37.3707989730854,37.8653718652017,38.3599447573179,38.8545176494342,39.3490905415504,
39.8436634336667,40.3382363257829,40.8328092178991,40.8407044966673),
 .UNSPECIFIED.);
#463=B_SPLINE_CURVE_WITH_KNOTS('',3,(#22244,#22245,#22246,#22247,#22248,
#22249,#22250,#22251,#22252,#22253,#22254,#22255,#22256,#22257,#22258,#22259),
 .UNSPECIFIED.,.F.,.F.,(4,1,1,1,1,1,1,1,1,1,1,1,1,4),(34.5575191894877,
34.9717768370047,35.4663497291209,35.9609226212372,36.4554955133534,36.9500684054697,
37.4446412975859,37.9392141897022,38.4337870818184,38.9283599739347,39.4229328660509,
39.9175057581671,40.4120786502834,40.8407044966673),.UNSPECIFIED.);
#464=B_SPLINE_CURVE_WITH_KNOTS('',3,(#22264,#22265,#22266,#22267,#22268,
#22269,#22270,#22271,#22272,#22273,#22274,#22275,#22276,#22277,#22278,#22279,
#22280),.UNSPECIFIED.,.F.,.F.,(4,1,1,1,1,1,1,1,1,1,1,1,1,1,4),(28.2743338823081,
28.468486914993,28.9630598071093,29.4576326992255,29.9522055913417,30.446778483458,
30.9413513755742,31.4359242676905,31.9304971598067,32.425070051923,32.9196429440392,
33.4142158361555,33.9087887282717,34.403361620388,34.5575191894877),
 .UNSPECIFIED.);
#465=B_SPLINE_CURVE_WITH_KNOTS('',3,(#22281,#22282,#22283,#22284,#22285,
#22286,#22287,#22288,#22289,#22290,#22291,#22292,#22293,#22294,#22295,#22296,
#22297),.UNSPECIFIED.,.F.,.F.,(4,1,1,1,1,1,1,1,1,1,1,1,1,1,4),(28.2743338823081,
28.5423292394935,29.0369021316097,29.531475023726,30.0260479158422,30.5206208079585,
31.0151937000747,31.509766592191,32.0043394843072,32.4989123764235,32.9934852685397,
33.488058160656,33.9826310527722,34.4772039448884,34.5575191894877),
 .UNSPECIFIED.);
#466=B_SPLINE_CURVE_WITH_KNOTS('',3,(#22302,#22303,#22304,#22305,#22306,
#22307,#22308,#22309,#22310,#22311,#22312,#22313,#22314,#22315,#22316,#22317,
#22318),.UNSPECIFIED.,.F.,.F.,(4,1,1,1,1,1,1,1,1,1,1,1,1,1,4),(21.9911485751285,
22.0390393174818,22.5336122095981,23.0281851017143,23.5227579938306,24.0173308859468,
24.511903778063,25.0064766701793,25.5010495622955,25.9956224544118,26.490195346528,
26.9847682386443,27.4793411307605,27.9739140228768,28.2743338823081),
 .UNSPECIFIED.);
#467=B_SPLINE_CURVE_WITH_KNOTS('',3,(#22319,#22320,#22321,#22322,#22323,
#22324,#22325,#22326,#22327,#22328,#22329,#22330,#22331,#22332,#22333,#22334,
#22335),.UNSPECIFIED.,.F.,.F.,(4,1,1,1,1,1,1,1,1,1,1,1,1,1,4),(21.9911485751285,
22.1128816419823,22.6074545340986,23.1020274262148,23.596600318331,24.0911732104473,
24.5857461025635,25.0803189946798,25.574891886796,26.0694647789123,26.5640376710285,
27.0586105631448,27.553183455261,28.0477563473773,28.2743338823081),
 .UNSPECIFIED.);
#468=B_SPLINE_CURVE_WITH_KNOTS('',3,(#22341,#22342,#22343,#22344,#22345),
 .UNSPECIFIED.,.F.,.F.,(4,1,4),(15.1888611523549,15.6834340444711,15.7079632679489),
 .UNSPECIFIED.);
#469=B_SPLINE_CURVE_WITH_KNOTS('',3,(#22348,#22349,#22350,#22351,#22352,
#22353,#22354,#22355,#22356,#22357),.UNSPECIFIED.,.F.,.F.,(4,1,1,1,1,1,
1,4),(13.0854727299533,13.1367272593894,13.6313001515056,14.1258730436219,
14.6204459357381,15.1150188278544,15.6095917199706,15.7079632679489),
 .UNSPECIFIED.);
#470=B_SPLINE_CURVE_WITH_KNOTS('',3,(#22359,#22360,#22361,#22362,#22363,
#22364,#22365,#22366,#22367,#22368,#22369,#22370,#22371,#22372,#22373,#22374),
 .UNSPECIFIED.,.F.,.F.,(4,1,1,1,1,1,1,1,1,1,1,1,1,4),(15.7079632679489,
16.1041646120869,16.5987375042031,17.0933103963194,17.5878832884356,18.0824561805519,
18.5770290726681,19.0716019647843,19.5661748569006,20.0607477490168,20.5553206411331,
21.0498935332493,21.5444664253656,21.9911485751285),.UNSPECIFIED.);
#471=B_SPLINE_CURVE_WITH_KNOTS('',3,(#22375,#22376,#22377,#22378,#22379,
#22380,#22381,#22382,#22383,#22384,#22385,#22386,#22387,#22388,#22389,#22390),
 .UNSPECIFIED.,.F.,.F.,(4,1,1,1,1,1,1,1,1,1,1,1,1,4),(15.7079632679489,
16.1780069365874,16.6725798287036,17.1671527208199,17.6617256129361,18.1562985050523,
18.6508713971686,19.1454442892848,19.6400171814011,20.1345900735173,20.6291629656336,
21.1237358577498,21.6183087498661,21.9911485751285),.UNSPECIFIED.);
#472=B_SPLINE_CURVE_WITH_KNOTS('',3,(#22851,#22852,#22853,#22854,#22855,
#22856,#22857,#22858,#22859,#22860,#22861,#22862,#22863,#22864,#22865,#22866,
#22867,#22868,#22869,#22870,#22871,#22872,#22873,#22874,#22875,#22876,#22877,
#22878,#22879,#22880,#22881),.UNSPECIFIED.,.F.,.F.,(4,3,3,3,3,3,3,3,3,3,
4),(0.,0.0822466706468383,0.162608105240606,0.216579893838171,0.23924274204394,
0.301838371937517,0.36076250940623,0.388067588559334,0.409537377502954,
0.476290104322315,0.53753492181237),.UNSPECIFIED.);
#473=B_SPLINE_CURVE_WITH_KNOTS('',3,(#22882,#22883,#22884,#22885,#22886,
#22887,#22888,#22889,#22890,#22891,#22892,#22893,#22894,#22895,#22896,#22897,
#22898,#22899,#22900,#22901,#22902,#22903,#22904,#22905,#22906,#22907,#22908,
#22909),.UNSPECIFIED.,.F.,.F.,(4,3,3,3,3,3,3,3,3,4),(0.,0.0665230127441691,
0.13429495842692,0.176258819244205,0.195926107024299,0.263526952009386,
0.33682854572103,0.365338415901403,0.449700157257057,0.534061898612711),
 .UNSPECIFIED.);
#474=B_SPLINE_CURVE_WITH_KNOTS('',3,(#22910,#22911,#22912,#22913,#22914,
#22915,#22916,#22917,#22918,#22919,#22920,#22921,#22922,#22923,#22924,#22925,
#22926,#22927,#22928,#22929,#22930,#22931,#22932,#22933,#22934,#22935,#22936,
#22937,#22938,#22939,#22940,#22941,#22942,#22943,#22944,#22945,#22946,#22947,
#22948,#22949),.UNSPECIFIED.,.F.,.F.,(4,3,3,3,3,3,3,3,3,3,3,3,3,4),(-53.8258642502287,
-53.4138723485545,-52.9192994564383,-52.424726564322,-51.9301536722058,
-51.4355807800895,-50.9410078879733,-50.446434995857,-49.9518621037408,
-49.4572892116245,-48.9627163195083,-48.4681434273921,-47.9735705352758,
-47.5426789430491),.UNSPECIFIED.);
#475=B_SPLINE_CURVE_WITH_KNOTS('',3,(#23411,#23412,#23413,#23414,#23415,
#23416,#23417,#23418,#23419,#23420,#23421,#23422,#23423,#23424,#23425,#23426,
#23427,#23428,#23429,#23430,#23431,#23432,#23433,#23434,#23435,#23436,#23437,
#23438),.UNSPECIFIED.,.F.,.F.,(4,3,3,3,3,3,3,3,3,4),(0.,0.0665230199567328,
0.134294967830964,0.176258831509978,0.195926124443112,0.263526952009376,
0.336828549458816,0.365338416771381,0.449700157692121,0.534061898612861),
 .UNSPECIFIED.);
#476=B_SPLINE_CURVE_WITH_KNOTS('',3,(#23439,#23440,#23441,#23442,#23443,
#23444,#23445,#23446,#23447,#23448,#23449,#23450,#23451,#23452,#23453,#23454,
#23455,#23456,#23457,#23458,#23459,#23460,#23461,#23462,#23463,#23464,#23465,
#23466,#23467,#23468,#23469),.UNSPECIFIED.,.F.,.F.,(4,3,3,3,3,3,3,3,3,3,
4),(50.7845845730308,50.9410078879733,51.4355807800895,51.9301536722058,
52.424726564322,52.9192994564383,53.4138723485545,53.9084452406708,54.403018132787,
54.8975910249033,55.3921639170195),.UNSPECIFIED.);
#477=B_SPLINE_CURVE_WITH_KNOTS('',3,(#23470,#23471,#23472,#23473,#23474,
#23475,#23476,#23477,#23478,#23479,#23480,#23481,#23482,#23483,#23484,#23485,
#23486,#23487,#23488,#23489,#23490,#23491,#23492,#23493,#23494,#23495,#23496,
#23497,#23498,#23499,#23500),.UNSPECIFIED.,.F.,.F.,(4,3,3,3,3,3,3,3,3,3,
4),(0.,0.0822466663612967,0.162608100396307,0.216579890867136,0.239242742625966,
0.301838371937549,0.360762509406336,0.388067584071394,0.409537375230468,
0.476290092032249,0.537534921812695),.UNSPECIFIED.);
#842=SHAPE_REPRESENTATION_RELATIONSHIP('SRR','None',#34219,#886);
#886=ADVANCED_BREP_SHAPE_REPRESENTATION('',(#1002),#33967);
#945=STYLED_ITEM('',(#34524),#1002);
#1002=MANIFOLD_SOLID_BREP('Body1',#13058);
#1193=FACE_BOUND('',#2941,.T.);
#1194=FACE_BOUND('',#2942,.T.);
#1195=FACE_BOUND('',#2943,.T.);
#1196=FACE_BOUND('',#2944,.T.);
#1197=FACE_BOUND('',#2950,.T.);
#1198=FACE_BOUND('',#2951,.T.);
#1199=FACE_BOUND('',#2952,.T.);
#1200=FACE_BOUND('',#2953,.T.);
#1201=FACE_BOUND('',#2958,.T.);
#1489=PLANE('',#14452);
#1490=PLANE('',#14464);
#1491=PLANE('',#14465);
#1492=PLANE('',#14472);
#2015=FACE_OUTER_BOUND('',#2919,.T.);
#2016=FACE_OUTER_BOUND('',#2920,.T.);
#2017=FACE_OUTER_BOUND('',#2921,.T.);
#2018=FACE_OUTER_BOUND('',#2922,.T.);
#2019=FACE_OUTER_BOUND('',#2923,.T.);
#2020=FACE_OUTER_BOUND('',#2924,.T.);
#2021=FACE_OUTER_BOUND('',#2925,.T.);
#2022=FACE_OUTER_BOUND('',#2926,.T.);
#2023=FACE_OUTER_BOUND('',#2927,.T.);
#2024=FACE_OUTER_BOUND('',#2928,.T.);
#2025=FACE_OUTER_BOUND('',#2929,.T.);
#2026=FACE_OUTER_BOUND('',#2930,.T.);
#2027=FACE_OUTER_BOUND('',#2931,.T.);
#2028=FACE_OUTER_BOUND('',#2932,.T.);
#2029=FACE_OUTER_BOUND('',#2933,.T.);
#2030=FACE_OUTER_BOUND('',#2934,.T.);
#2031=FACE_OUTER_BOUND('',#2935,.T.);
#2032=FACE_OUTER_BOUND('',#2936,.T.);
#2033=FACE_OUTER_BOUND('',#2937,.T.);
#2034=FACE_OUTER_BOUND('',#2938,.T.);
#2035=FACE_OUTER_BOUND('',#2939,.T.);
#2036=FACE_OUTER_BOUND('',#2940,.T.);
#2037=FACE_OUTER_BOUND('',#2945,.T.);
#2038=FACE_OUTER_BOUND('',#2946,.T.);
#2039=FACE_OUTER_BOUND('',#2947,.T.);
#2040=FACE_OUTER_BOUND('',#2948,.T.);
#2041=FACE_OUTER_BOUND('',#2949,.T.);
#2042=FACE_OUTER_BOUND('',#2954,.T.);
#2043=FACE_OUTER_BOUND('',#2955,.T.);
#2044=FACE_OUTER_BOUND('',#2956,.T.);
#2045=FACE_OUTER_BOUND('',#2957,.T.);
#2919=EDGE_LOOP('',(#10551,#10552,#10553,#10554));
#2920=EDGE_LOOP('',(#10555,#10556,#10557,#10558));
#2921=EDGE_LOOP('',(#10559,#10560,#10561,#10562));
#2922=EDGE_LOOP('',(#10563,#10564,#10565,#10566));
#2923=EDGE_LOOP('',(#10567,#10568,#10569,#10570));
#2924=EDGE_LOOP('',(#10571,#10572,#10573,#10574));
#2925=EDGE_LOOP('',(#10575,#10576,#10577,#10578));
#2926=EDGE_LOOP('',(#10579,#10580,#10581,#10582));
#2927=EDGE_LOOP('',(#10583,#10584,#10585));
#2928=EDGE_LOOP('',(#10586,#10587,#10588,#10589));
#2929=EDGE_LOOP('',(#10590,#10591,#10592,#10593));
#2930=EDGE_LOOP('',(#10594,#10595,#10596,#10597));
#2931=EDGE_LOOP('',(#10598,#10599,#10600,#10601));
#2932=EDGE_LOOP('',(#10602,#10603,#10604,#10605));
#2933=EDGE_LOOP('',(#10606,#10607,#10608,#10609));
#2934=EDGE_LOOP('',(#10610,#10611,#10612,#10613));
#2935=EDGE_LOOP('',(#10614,#10615,#10616,#10617));
#2936=EDGE_LOOP('',(#10618,#10619,#10620,#10621));
#2937=EDGE_LOOP('',(#10622,#10623,#10624,#10625));
#2938=EDGE_LOOP('',(#10626,#10627,#10628,#10629,#10630,#10631,#10632,#10633,
#10634,#10635,#10636,#10637,#10638,#10639,#10640,#10641,#10642,#10643,#10644,
#10645,#10646,#10647));
#2939=EDGE_LOOP('',(#10648,#10649,#10650,#10651,#10652,#10653,#10654,#10655,
#10656,#10657,#10658,#10659,#10660,#10661,#10662,#10663,#10664,#10665,#10666,
#10667,#10668));
#2940=EDGE_LOOP('',(#10669,#10670));
#2941=EDGE_LOOP('',(#10671,#10672,#10673,#10674,#10675));
#2942=EDGE_LOOP('',(#10676));
#2943=EDGE_LOOP('',(#10677));
#2944=EDGE_LOOP('',(#10678));
#2945=EDGE_LOOP('',(#10679,#10680,#10681,#10682));
#2946=EDGE_LOOP('',(#10683,#10684,#10685,#10686));
#2947=EDGE_LOOP('',(#10687,#10688,#10689,#10690));
#2948=EDGE_LOOP('',(#10691,#10692,#10693,#10694));
#2949=EDGE_LOOP('',(#10695,#10696));
#2950=EDGE_LOOP('',(#10697));
#2951=EDGE_LOOP('',(#10698));
#2952=EDGE_LOOP('',(#10699));
#2953=EDGE_LOOP('',(#10700));
#2954=EDGE_LOOP('',(#10701,#10702,#10703,#10704));
#2955=EDGE_LOOP('',(#10705,#10706,#10707,#10708,#10709));
#2956=EDGE_LOOP('',(#10710,#10711,#10712,#10713));
#2957=EDGE_LOOP('',(#10714));
#2958=EDGE_LOOP('',(#10715,#10716,#10717,#10718));
#3857=LINE('',#21345,#4791);
#3858=LINE('',#21417,#4792);
#3859=LINE('',#21504,#4793);
#3860=LINE('',#21594,#4794);
#3861=LINE('',#21681,#4795);
#3862=LINE('',#21771,#4796);
#3863=LINE('',#21858,#4797);
#3864=LINE('',#21945,#4798);
#3865=LINE('',#22035,#4799);
#3866=LINE('',#22051,#4800);
#3867=LINE('',#22077,#4801);
#3868=LINE('',#22114,#4802);
#3869=LINE('',#22151,#4803);
#3870=LINE('',#22189,#4804);
#3871=LINE('',#22226,#4805);
#3872=LINE('',#22263,#4806);
#3873=LINE('',#22301,#4807);
#3874=LINE('',#22339,#4808);
#3875=LINE('',#23504,#4809);
#3876=LINE('',#23516,#4810);
#3877=LINE('',#23520,#4811);
#3878=LINE('',#23524,#4812);
#3879=LINE('',#23528,#4813);
#3880=LINE('',#23529,#4814);
#3881=LINE('',#23530,#4815);
#3882=LINE('',#23539,#4816);
#4791=VECTOR('',#17252,0.45);
#4792=VECTOR('',#17257,0.45);
#4793=VECTOR('',#17260,0.45);
#4794=VECTOR('',#17263,0.45);
#4795=VECTOR('',#17266,0.45);
#4796=VECTOR('',#17269,0.45);
#4797=VECTOR('',#17272,0.45);
#4798=VECTOR('',#17275,0.45);
#4799=VECTOR('',#17278,0.45);
#4800=VECTOR('',#17283,0.625);
#4801=VECTOR('',#17288,0.625);
#4802=VECTOR('',#17291,0.625);
#4803=VECTOR('',#17294,0.625);
#4804=VECTOR('',#17297,0.625);
#4805=VECTOR('',#17300,0.625);
#4806=VECTOR('',#17303,0.625);
#4807=VECTOR('',#17306,0.625);
#4808=VECTOR('',#17309,0.625);
#4809=VECTOR('',#17316,1.);
#4810=VECTOR('',#17331,0.225);
#4811=VECTOR('',#17336,0.225);
#4812=VECTOR('',#17341,0.225);
#4813=VECTOR('',#17344,1.);
#4814=VECTOR('',#17345,1.);
#4815=VECTOR('',#17346,1.);
#4816=VECTOR('',#17359,1.1);
#5482=CIRCLE('',#14430,0.457875);
#5483=CIRCLE('',#14439,0.457875);
#5484=CIRCLE('',#14441,0.625);
#5485=CIRCLE('',#14450,0.625);
#5486=CIRCLE('',#14453,1.9);
#5487=CIRCLE('',#14454,0.457875);
#5488=CIRCLE('',#14455,0.225);
#5489=CIRCLE('',#14456,0.225);
#5490=CIRCLE('',#14457,0.225);
#5491=CIRCLE('',#14459,0.225);
#5492=CIRCLE('',#14461,0.225);
#5493=CIRCLE('',#14463,0.225);
#5494=CIRCLE('',#14466,1.9);
#5495=CIRCLE('',#14467,1.1);
#5496=CIRCLE('',#14471,1.1);
#6272=VERTEX_POINT('',#21343);
#6273=VERTEX_POINT('',#21344);
#6274=VERTEX_POINT('',#21346);
#6275=VERTEX_POINT('',#21372);
#6276=VERTEX_POINT('',#21415);
#6277=VERTEX_POINT('',#21416);
#6278=VERTEX_POINT('',#21502);
#6279=VERTEX_POINT('',#21503);
#6280=VERTEX_POINT('',#21592);
#6281=VERTEX_POINT('',#21593);
#6282=VERTEX_POINT('',#21679);
#6283=VERTEX_POINT('',#21680);
#6284=VERTEX_POINT('',#21769);
#6285=VERTEX_POINT('',#21770);
#6286=VERTEX_POINT('',#21856);
#6287=VERTEX_POINT('',#21857);
#6288=VERTEX_POINT('',#21943);
#6289=VERTEX_POINT('',#21944);
#6290=VERTEX_POINT('',#22033);
#6291=VERTEX_POINT('',#22034);
#6292=VERTEX_POINT('',#22036);
#6293=VERTEX_POINT('',#22049);
#6294=VERTEX_POINT('',#22050);
#6295=VERTEX_POINT('',#22052);
#6296=VERTEX_POINT('',#22060);
#6297=VERTEX_POINT('',#22075);
#6298=VERTEX_POINT('',#22076);
#6299=VERTEX_POINT('',#22112);
#6300=VERTEX_POINT('',#22113);
#6301=VERTEX_POINT('',#22149);
#6302=VERTEX_POINT('',#22150);
#6303=VERTEX_POINT('',#22187);
#6304=VERTEX_POINT('',#22188);
#6305=VERTEX_POINT('',#22224);
#6306=VERTEX_POINT('',#22225);
#6307=VERTEX_POINT('',#22261);
#6308=VERTEX_POINT('',#22262);
#6309=VERTEX_POINT('',#22299);
#6310=VERTEX_POINT('',#22300);
#6311=VERTEX_POINT('',#22337);
#6312=VERTEX_POINT('',#22338);
#6313=VERTEX_POINT('',#22340);
#6314=VERTEX_POINT('',#22346);
#6315=VERTEX_POINT('',#23410);
#6316=VERTEX_POINT('',#23502);
#6317=VERTEX_POINT('',#23503);
#6318=VERTEX_POINT('',#23507);
#6319=VERTEX_POINT('',#23509);
#6320=VERTEX_POINT('',#23511);
#6321=VERTEX_POINT('',#23514);
#6322=VERTEX_POINT('',#23518);
#6323=VERTEX_POINT('',#23522);
#6324=VERTEX_POINT('',#23526);
#6325=VERTEX_POINT('',#23527);
#6326=VERTEX_POINT('',#23533);
#6327=VERTEX_POINT('',#23538);
#7775=EDGE_CURVE('',#6272,#6273,#3857,.T.);
#7776=EDGE_CURVE('',#6273,#6274,#435,.T.);
#7777=EDGE_CURVE('',#6274,#6275,#5482,.F.);
#7778=EDGE_CURVE('',#6275,#6272,#436,.T.);
#7779=EDGE_CURVE('',#6276,#6277,#3858,.T.);
#7780=EDGE_CURVE('',#6277,#6273,#437,.T.);
#7781=EDGE_CURVE('',#6272,#6276,#438,.T.);
#7782=EDGE_CURVE('',#6278,#6279,#3859,.T.);
#7783=EDGE_CURVE('',#6279,#6277,#439,.T.);
#7784=EDGE_CURVE('',#6276,#6278,#440,.T.);
#7785=EDGE_CURVE('',#6280,#6281,#3860,.T.);
#7786=EDGE_CURVE('',#6281,#6279,#441,.T.);
#7787=EDGE_CURVE('',#6278,#6280,#442,.T.);
#7788=EDGE_CURVE('',#6282,#6283,#3861,.T.);
#7789=EDGE_CURVE('',#6283,#6281,#443,.T.);
#7790=EDGE_CURVE('',#6280,#6282,#444,.T.);
#7791=EDGE_CURVE('',#6284,#6285,#3862,.T.);
#7792=EDGE_CURVE('',#6285,#6283,#445,.T.);
#7793=EDGE_CURVE('',#6282,#6284,#446,.T.);
#7794=EDGE_CURVE('',#6286,#6287,#3863,.T.);
#7795=EDGE_CURVE('',#6287,#6285,#447,.T.);
#7796=EDGE_CURVE('',#6284,#6286,#448,.T.);
#7797=EDGE_CURVE('',#6288,#6289,#3864,.T.);
#7798=EDGE_CURVE('',#6289,#6287,#449,.T.);
#7799=EDGE_CURVE('',#6286,#6288,#450,.T.);
#7800=EDGE_CURVE('',#6290,#6291,#3865,.T.);
#7801=EDGE_CURVE('',#6292,#6290,#5483,.F.);
#7802=EDGE_CURVE('',#6292,#6291,#451,.T.);
#7803=EDGE_CURVE('',#6293,#6294,#3866,.T.);
#7804=EDGE_CURVE('',#6294,#6295,#452,.T.);
#7805=EDGE_CURVE('',#6296,#6295,#5484,.T.);
#7806=EDGE_CURVE('',#6293,#6296,#453,.T.);
#7807=EDGE_CURVE('',#6297,#6298,#3867,.T.);
#7808=EDGE_CURVE('',#6298,#6294,#454,.T.);
#7809=EDGE_CURVE('',#6297,#6293,#455,.T.);
#7810=EDGE_CURVE('',#6299,#6300,#3868,.T.);
#7811=EDGE_CURVE('',#6300,#6298,#456,.T.);
#7812=EDGE_CURVE('',#6299,#6297,#457,.T.);
#7813=EDGE_CURVE('',#6301,#6302,#3869,.T.);
#7814=EDGE_CURVE('',#6302,#6300,#458,.T.);
#7815=EDGE_CURVE('',#6301,#6299,#459,.T.);
#7816=EDGE_CURVE('',#6303,#6304,#3870,.T.);
#7817=EDGE_CURVE('',#6304,#6302,#460,.T.);
#7818=EDGE_CURVE('',#6303,#6301,#461,.T.);
#7819=EDGE_CURVE('',#6305,#6306,#3871,.T.);
#7820=EDGE_CURVE('',#6306,#6304,#462,.T.);
#7821=EDGE_CURVE('',#6305,#6303,#463,.T.);
#7822=EDGE_CURVE('',#6307,#6308,#3872,.T.);
#7823=EDGE_CURVE('',#6308,#6306,#464,.T.);
#7824=EDGE_CURVE('',#6307,#6305,#465,.T.);
#7825=EDGE_CURVE('',#6309,#6310,#3873,.T.);
#7826=EDGE_CURVE('',#6310,#6308,#466,.T.);
#7827=EDGE_CURVE('',#6309,#6307,#467,.T.);
#7828=EDGE_CURVE('',#6311,#6312,#3874,.T.);
#7829=EDGE_CURVE('',#6313,#6311,#468,.T.);
#7830=EDGE_CURVE('',#6314,#6313,#5485,.T.);
#7831=EDGE_CURVE('',#6314,#6312,#469,.T.);
#7832=EDGE_CURVE('',#6312,#6310,#470,.T.);
#7833=EDGE_CURVE('',#6311,#6309,#471,.T.);
#7834=EDGE_CURVE('',#6295,#6292,#472,.T.);
#7835=EDGE_CURVE('',#6274,#6314,#473,.T.);
#7836=EDGE_CURVE('',#6291,#6289,#474,.T.);
#7837=EDGE_CURVE('',#6315,#6296,#475,.T.);
#7838=EDGE_CURVE('',#6288,#6315,#476,.T.);
#7839=EDGE_CURVE('',#6313,#6275,#477,.T.);
#7840=EDGE_CURVE('',#6316,#6317,#3875,.T.);
#7841=EDGE_CURVE('',#6317,#6316,#5486,.T.);
#7842=EDGE_CURVE('',#6290,#6315,#5487,.F.);
#7843=EDGE_CURVE('',#6318,#6318,#5488,.T.);
#7844=EDGE_CURVE('',#6319,#6319,#5489,.T.);
#7845=EDGE_CURVE('',#6320,#6320,#5490,.T.);
#7846=EDGE_CURVE('',#6321,#6321,#5491,.T.);
#7847=EDGE_CURVE('',#6321,#6320,#3876,.T.);
#7848=EDGE_CURVE('',#6322,#6322,#5492,.T.);
#7849=EDGE_CURVE('',#6322,#6319,#3877,.T.);
#7850=EDGE_CURVE('',#6323,#6323,#5493,.T.);
#7851=EDGE_CURVE('',#6323,#6318,#3878,.T.);
#7852=EDGE_CURVE('',#6324,#6325,#3879,.T.);
#7853=EDGE_CURVE('',#6317,#6324,#3880,.T.);
#7854=EDGE_CURVE('',#6325,#6316,#3881,.T.);
#7855=EDGE_CURVE('',#6324,#6325,#5494,.T.);
#7856=EDGE_CURVE('',#6326,#6326,#5495,.T.);
#7857=EDGE_CURVE('',#6326,#6327,#3882,.T.);
#7858=EDGE_CURVE('',#6327,#6327,#5496,.T.);
#10551=ORIENTED_EDGE('',*,*,#7775,.T.);
#10552=ORIENTED_EDGE('',*,*,#7776,.T.);
#10553=ORIENTED_EDGE('',*,*,#7777,.T.);
#10554=ORIENTED_EDGE('',*,*,#7778,.T.);
#10555=ORIENTED_EDGE('',*,*,#7779,.T.);
#10556=ORIENTED_EDGE('',*,*,#7780,.T.);
#10557=ORIENTED_EDGE('',*,*,#7775,.F.);
#10558=ORIENTED_EDGE('',*,*,#7781,.T.);
#10559=ORIENTED_EDGE('',*,*,#7782,.T.);
#10560=ORIENTED_EDGE('',*,*,#7783,.T.);
#10561=ORIENTED_EDGE('',*,*,#7779,.F.);
#10562=ORIENTED_EDGE('',*,*,#7784,.T.);
#10563=ORIENTED_EDGE('',*,*,#7785,.T.);
#10564=ORIENTED_EDGE('',*,*,#7786,.T.);
#10565=ORIENTED_EDGE('',*,*,#7782,.F.);
#10566=ORIENTED_EDGE('',*,*,#7787,.T.);
#10567=ORIENTED_EDGE('',*,*,#7788,.T.);
#10568=ORIENTED_EDGE('',*,*,#7789,.T.);
#10569=ORIENTED_EDGE('',*,*,#7785,.F.);
#10570=ORIENTED_EDGE('',*,*,#7790,.T.);
#10571=ORIENTED_EDGE('',*,*,#7791,.T.);
#10572=ORIENTED_EDGE('',*,*,#7792,.T.);
#10573=ORIENTED_EDGE('',*,*,#7788,.F.);
#10574=ORIENTED_EDGE('',*,*,#7793,.T.);
#10575=ORIENTED_EDGE('',*,*,#7794,.T.);
#10576=ORIENTED_EDGE('',*,*,#7795,.T.);
#10577=ORIENTED_EDGE('',*,*,#7791,.F.);
#10578=ORIENTED_EDGE('',*,*,#7796,.T.);
#10579=ORIENTED_EDGE('',*,*,#7797,.T.);
#10580=ORIENTED_EDGE('',*,*,#7798,.T.);
#10581=ORIENTED_EDGE('',*,*,#7794,.F.);
#10582=ORIENTED_EDGE('',*,*,#7799,.T.);
#10583=ORIENTED_EDGE('',*,*,#7800,.F.);
#10584=ORIENTED_EDGE('',*,*,#7801,.F.);
#10585=ORIENTED_EDGE('',*,*,#7802,.T.);
#10586=ORIENTED_EDGE('',*,*,#7803,.T.);
#10587=ORIENTED_EDGE('',*,*,#7804,.T.);
#10588=ORIENTED_EDGE('',*,*,#7805,.F.);
#10589=ORIENTED_EDGE('',*,*,#7806,.F.);
#10590=ORIENTED_EDGE('',*,*,#7807,.T.);
#10591=ORIENTED_EDGE('',*,*,#7808,.T.);
#10592=ORIENTED_EDGE('',*,*,#7803,.F.);
#10593=ORIENTED_EDGE('',*,*,#7809,.F.);
#10594=ORIENTED_EDGE('',*,*,#7810,.T.);
#10595=ORIENTED_EDGE('',*,*,#7811,.T.);
#10596=ORIENTED_EDGE('',*,*,#7807,.F.);
#10597=ORIENTED_EDGE('',*,*,#7812,.F.);
#10598=ORIENTED_EDGE('',*,*,#7813,.T.);
#10599=ORIENTED_EDGE('',*,*,#7814,.T.);
#10600=ORIENTED_EDGE('',*,*,#7810,.F.);
#10601=ORIENTED_EDGE('',*,*,#7815,.F.);
#10602=ORIENTED_EDGE('',*,*,#7816,.T.);
#10603=ORIENTED_EDGE('',*,*,#7817,.T.);
#10604=ORIENTED_EDGE('',*,*,#7813,.F.);
#10605=ORIENTED_EDGE('',*,*,#7818,.F.);
#10606=ORIENTED_EDGE('',*,*,#7819,.T.);
#10607=ORIENTED_EDGE('',*,*,#7820,.T.);
#10608=ORIENTED_EDGE('',*,*,#7816,.F.);
#10609=ORIENTED_EDGE('',*,*,#7821,.F.);
#10610=ORIENTED_EDGE('',*,*,#7822,.T.);
#10611=ORIENTED_EDGE('',*,*,#7823,.T.);
#10612=ORIENTED_EDGE('',*,*,#7819,.F.);
#10613=ORIENTED_EDGE('',*,*,#7824,.F.);
#10614=ORIENTED_EDGE('',*,*,#7825,.T.);
#10615=ORIENTED_EDGE('',*,*,#7826,.T.);
#10616=ORIENTED_EDGE('',*,*,#7822,.F.);
#10617=ORIENTED_EDGE('',*,*,#7827,.F.);
#10618=ORIENTED_EDGE('',*,*,#7828,.F.);
#10619=ORIENTED_EDGE('',*,*,#7829,.F.);
#10620=ORIENTED_EDGE('',*,*,#7830,.F.);
#10621=ORIENTED_EDGE('',*,*,#7831,.T.);
#10622=ORIENTED_EDGE('',*,*,#7828,.T.);
#10623=ORIENTED_EDGE('',*,*,#7832,.T.);
#10624=ORIENTED_EDGE('',*,*,#7825,.F.);
#10625=ORIENTED_EDGE('',*,*,#7833,.F.);
#10626=ORIENTED_EDGE('',*,*,#7834,.F.);
#10627=ORIENTED_EDGE('',*,*,#7804,.F.);
#10628=ORIENTED_EDGE('',*,*,#7808,.F.);
#10629=ORIENTED_EDGE('',*,*,#7811,.F.);
#10630=ORIENTED_EDGE('',*,*,#7814,.F.);
#10631=ORIENTED_EDGE('',*,*,#7817,.F.);
#10632=ORIENTED_EDGE('',*,*,#7820,.F.);
#10633=ORIENTED_EDGE('',*,*,#7823,.F.);
#10634=ORIENTED_EDGE('',*,*,#7826,.F.);
#10635=ORIENTED_EDGE('',*,*,#7832,.F.);
#10636=ORIENTED_EDGE('',*,*,#7831,.F.);
#10637=ORIENTED_EDGE('',*,*,#7835,.F.);
#10638=ORIENTED_EDGE('',*,*,#7776,.F.);
#10639=ORIENTED_EDGE('',*,*,#7780,.F.);
#10640=ORIENTED_EDGE('',*,*,#7783,.F.);
#10641=ORIENTED_EDGE('',*,*,#7786,.F.);
#10642=ORIENTED_EDGE('',*,*,#7789,.F.);
#10643=ORIENTED_EDGE('',*,*,#7792,.F.);
#10644=ORIENTED_EDGE('',*,*,#7795,.F.);
#10645=ORIENTED_EDGE('',*,*,#7798,.F.);
#10646=ORIENTED_EDGE('',*,*,#7836,.F.);
#10647=ORIENTED_EDGE('',*,*,#7802,.F.);
#10648=ORIENTED_EDGE('',*,*,#7837,.F.);
#10649=ORIENTED_EDGE('',*,*,#7838,.F.);
#10650=ORIENTED_EDGE('',*,*,#7799,.F.);
#10651=ORIENTED_EDGE('',*,*,#7796,.F.);
#10652=ORIENTED_EDGE('',*,*,#7793,.F.);
#10653=ORIENTED_EDGE('',*,*,#7790,.F.);
#10654=ORIENTED_EDGE('',*,*,#7787,.F.);
#10655=ORIENTED_EDGE('',*,*,#7784,.F.);
#10656=ORIENTED_EDGE('',*,*,#7781,.F.);
#10657=ORIENTED_EDGE('',*,*,#7778,.F.);
#10658=ORIENTED_EDGE('',*,*,#7839,.F.);
#10659=ORIENTED_EDGE('',*,*,#7829,.T.);
#10660=ORIENTED_EDGE('',*,*,#7833,.T.);
#10661=ORIENTED_EDGE('',*,*,#7827,.T.);
#10662=ORIENTED_EDGE('',*,*,#7824,.T.);
#10663=ORIENTED_EDGE('',*,*,#7821,.T.);
#10664=ORIENTED_EDGE('',*,*,#7818,.T.);
#10665=ORIENTED_EDGE('',*,*,#7815,.T.);
#10666=ORIENTED_EDGE('',*,*,#7812,.T.);
#10667=ORIENTED_EDGE('',*,*,#7809,.T.);
#10668=ORIENTED_EDGE('',*,*,#7806,.T.);
#10669=ORIENTED_EDGE('',*,*,#7840,.T.);
#10670=ORIENTED_EDGE('',*,*,#7841,.T.);
#10671=ORIENTED_EDGE('',*,*,#7837,.T.);
#10672=ORIENTED_EDGE('',*,*,#7805,.T.);
#10673=ORIENTED_EDGE('',*,*,#7834,.T.);
#10674=ORIENTED_EDGE('',*,*,#7801,.T.);
#10675=ORIENTED_EDGE('',*,*,#7842,.T.);
#10676=ORIENTED_EDGE('',*,*,#7843,.T.);
#10677=ORIENTED_EDGE('',*,*,#7844,.T.);
#10678=ORIENTED_EDGE('',*,*,#7845,.T.);
#10679=ORIENTED_EDGE('',*,*,#7846,.F.);
#10680=ORIENTED_EDGE('',*,*,#7847,.T.);
#10681=ORIENTED_EDGE('',*,*,#7845,.F.);
#10682=ORIENTED_EDGE('',*,*,#7847,.F.);
#10683=ORIENTED_EDGE('',*,*,#7848,.F.);
#10684=ORIENTED_EDGE('',*,*,#7849,.T.);
#10685=ORIENTED_EDGE('',*,*,#7844,.F.);
#10686=ORIENTED_EDGE('',*,*,#7849,.F.);
#10687=ORIENTED_EDGE('',*,*,#7850,.F.);
#10688=ORIENTED_EDGE('',*,*,#7851,.T.);
#10689=ORIENTED_EDGE('',*,*,#7843,.F.);
#10690=ORIENTED_EDGE('',*,*,#7851,.F.);
#10691=ORIENTED_EDGE('',*,*,#7852,.F.);
#10692=ORIENTED_EDGE('',*,*,#7853,.F.);
#10693=ORIENTED_EDGE('',*,*,#7840,.F.);
#10694=ORIENTED_EDGE('',*,*,#7854,.F.);
#10695=ORIENTED_EDGE('',*,*,#7852,.T.);
#10696=ORIENTED_EDGE('',*,*,#7855,.F.);
#10697=ORIENTED_EDGE('',*,*,#7846,.T.);
#10698=ORIENTED_EDGE('',*,*,#7848,.T.);
#10699=ORIENTED_EDGE('',*,*,#7850,.T.);
#10700=ORIENTED_EDGE('',*,*,#7856,.T.);
#10701=ORIENTED_EDGE('',*,*,#7854,.T.);
#10702=ORIENTED_EDGE('',*,*,#7841,.F.);
#10703=ORIENTED_EDGE('',*,*,#7853,.T.);
#10704=ORIENTED_EDGE('',*,*,#7855,.T.);
#10705=ORIENTED_EDGE('',*,*,#7800,.T.);
#10706=ORIENTED_EDGE('',*,*,#7836,.T.);
#10707=ORIENTED_EDGE('',*,*,#7797,.F.);
#10708=ORIENTED_EDGE('',*,*,#7838,.T.);
#10709=ORIENTED_EDGE('',*,*,#7842,.F.);
#10710=ORIENTED_EDGE('',*,*,#7856,.F.);
#10711=ORIENTED_EDGE('',*,*,#7857,.T.);
#10712=ORIENTED_EDGE('',*,*,#7858,.T.);
#10713=ORIENTED_EDGE('',*,*,#7857,.F.);
#10714=ORIENTED_EDGE('',*,*,#7858,.F.);
#10715=ORIENTED_EDGE('',*,*,#7839,.T.);
#10716=ORIENTED_EDGE('',*,*,#7777,.F.);
#10717=ORIENTED_EDGE('',*,*,#7835,.T.);
#10718=ORIENTED_EDGE('',*,*,#7830,.T.);
#12108=CYLINDRICAL_SURFACE('',#14429,0.457875);
#12109=CYLINDRICAL_SURFACE('',#14431,0.457875);
#12110=CYLINDRICAL_SURFACE('',#14432,0.457875);
#12111=CYLINDRICAL_SURFACE('',#14433,0.457875);
#12112=CYLINDRICAL_SURFACE('',#14434,0.457875);
#12113=CYLINDRICAL_SURFACE('',#14435,0.457875);
#12114=CYLINDRICAL_SURFACE('',#14436,0.457875);
#12115=CYLINDRICAL_SURFACE('',#14437,0.457875);
#12116=CYLINDRICAL_SURFACE('',#14438,0.457875);
#12117=CYLINDRICAL_SURFACE('',#14440,0.625);
#12118=CYLINDRICAL_SURFACE('',#14442,0.625);
#12119=CYLINDRICAL_SURFACE('',#14443,0.625);
#12120=CYLINDRICAL_SURFACE('',#14444,0.625);
#12121=CYLINDRICAL_SURFACE('',#14445,0.625);
#12122=CYLINDRICAL_SURFACE('',#14446,0.625);
#12123=CYLINDRICAL_SURFACE('',#14447,0.625);
#12124=CYLINDRICAL_SURFACE('',#14448,0.625);
#12125=CYLINDRICAL_SURFACE('',#14449,0.625);
#12126=CYLINDRICAL_SURFACE('',#14451,0.625);
#12127=CYLINDRICAL_SURFACE('',#14458,0.225);
#12128=CYLINDRICAL_SURFACE('',#14460,0.225);
#12129=CYLINDRICAL_SURFACE('',#14462,0.225);
#12130=CYLINDRICAL_SURFACE('',#14468,1.9);
#12131=CYLINDRICAL_SURFACE('',#14469,0.457875);
#12132=CYLINDRICAL_SURFACE('',#14470,1.1);
#12727=ADVANCED_FACE('',(#2015),#12108,.F.);
#12728=ADVANCED_FACE('',(#2016),#12109,.F.);
#12729=ADVANCED_FACE('',(#2017),#12110,.F.);
#12730=ADVANCED_FACE('',(#2018),#12111,.F.);
#12731=ADVANCED_FACE('',(#2019),#12112,.F.);
#12732=ADVANCED_FACE('',(#2020),#12113,.F.);
#12733=ADVANCED_FACE('',(#2021),#12114,.F.);
#12734=ADVANCED_FACE('',(#2022),#12115,.F.);
#12735=ADVANCED_FACE('',(#2023),#12116,.F.);
#12736=ADVANCED_FACE('',(#2024),#12117,.F.);
#12737=ADVANCED_FACE('',(#2025),#12118,.F.);
#12738=ADVANCED_FACE('',(#2026),#12119,.F.);
#12739=ADVANCED_FACE('',(#2027),#12120,.F.);
#12740=ADVANCED_FACE('',(#2028),#12121,.F.);
#12741=ADVANCED_FACE('',(#2029),#12122,.F.);
#12742=ADVANCED_FACE('',(#2030),#12123,.F.);
#12743=ADVANCED_FACE('',(#2031),#12124,.F.);
#12744=ADVANCED_FACE('',(#2032),#12125,.F.);
#12745=ADVANCED_FACE('',(#2033),#12126,.F.);
#12746=ADVANCED_FACE('',(#2034),#11,.F.);
#12747=ADVANCED_FACE('',(#2035),#12,.F.);
#12748=ADVANCED_FACE('',(#2036,#1193,#1194,#1195,#1196),#1489,.T.);
#12749=ADVANCED_FACE('',(#2037),#12127,.F.);
#12750=ADVANCED_FACE('',(#2038),#12128,.F.);
#12751=ADVANCED_FACE('',(#2039),#12129,.F.);
#12752=ADVANCED_FACE('',(#2040),#1490,.F.);
#12753=ADVANCED_FACE('',(#2041,#1197,#1198,#1199,#1200),#1491,.F.);
#12754=ADVANCED_FACE('',(#2042),#12130,.T.);
#12755=ADVANCED_FACE('',(#2043),#12131,.F.);
#12756=ADVANCED_FACE('',(#2044),#12132,.T.);
#12757=ADVANCED_FACE('',(#2045,#1201),#1492,.F.);
#13058=CLOSED_SHELL('',(#12727,#12728,#12729,#12730,#12731,#12732,#12733,
#12734,#12735,#12736,#12737,#12738,#12739,#12740,#12741,#12742,#12743,#12744,
#12745,#12746,#12747,#12748,#12749,#12750,#12751,#12752,#12753,#12754,#12755,
#12756,#12757));
#14428=AXIS2_PLACEMENT_3D('',#21341,#17248,#17249);
#14429=AXIS2_PLACEMENT_3D('',#21342,#17250,#17251);
#14430=AXIS2_PLACEMENT_3D('',#21373,#17253,#17254);
#14431=AXIS2_PLACEMENT_3D('',#21414,#17255,#17256);
#14432=AXIS2_PLACEMENT_3D('',#21501,#17258,#17259);
#14433=AXIS2_PLACEMENT_3D('',#21591,#17261,#17262);
#14434=AXIS2_PLACEMENT_3D('',#21678,#17264,#17265);
#14435=AXIS2_PLACEMENT_3D('',#21768,#17267,#17268);
#14436=AXIS2_PLACEMENT_3D('',#21855,#17270,#17271);
#14437=AXIS2_PLACEMENT_3D('',#21942,#17273,#17274);
#14438=AXIS2_PLACEMENT_3D('',#22032,#17276,#17277);
#14439=AXIS2_PLACEMENT_3D('',#22037,#17279,#17280);
#14440=AXIS2_PLACEMENT_3D('',#22048,#17281,#17282);
#14441=AXIS2_PLACEMENT_3D('',#22061,#17284,#17285);
#14442=AXIS2_PLACEMENT_3D('',#22074,#17286,#17287);
#14443=AXIS2_PLACEMENT_3D('',#22111,#17289,#17290);
#14444=AXIS2_PLACEMENT_3D('',#22148,#17292,#17293);
#14445=AXIS2_PLACEMENT_3D('',#22186,#17295,#17296);
#14446=AXIS2_PLACEMENT_3D('',#22223,#17298,#17299);
#14447=AXIS2_PLACEMENT_3D('',#22260,#17301,#17302);
#14448=AXIS2_PLACEMENT_3D('',#22298,#17304,#17305);
#14449=AXIS2_PLACEMENT_3D('',#22336,#17307,#17308);
#14450=AXIS2_PLACEMENT_3D('',#22347,#17310,#17311);
#14451=AXIS2_PLACEMENT_3D('',#22358,#17312,#17313);
#14452=AXIS2_PLACEMENT_3D('',#23501,#17314,#17315);
#14453=AXIS2_PLACEMENT_3D('',#23505,#17317,#17318);
#14454=AXIS2_PLACEMENT_3D('',#23506,#17319,#17320);
#14455=AXIS2_PLACEMENT_3D('',#23508,#17321,#17322);
#14456=AXIS2_PLACEMENT_3D('',#23510,#17323,#17324);
#14457=AXIS2_PLACEMENT_3D('',#23512,#17325,#17326);
#14458=AXIS2_PLACEMENT_3D('',#23513,#17327,#17328);
#14459=AXIS2_PLACEMENT_3D('',#23515,#17329,#17330);
#14460=AXIS2_PLACEMENT_3D('',#23517,#17332,#17333);
#14461=AXIS2_PLACEMENT_3D('',#23519,#17334,#17335);
#14462=AXIS2_PLACEMENT_3D('',#23521,#17337,#17338);
#14463=AXIS2_PLACEMENT_3D('',#23523,#17339,#17340);
#14464=AXIS2_PLACEMENT_3D('',#23525,#17342,#17343);
#14465=AXIS2_PLACEMENT_3D('',#23531,#17347,#17348);
#14466=AXIS2_PLACEMENT_3D('',#23532,#17349,#17350);
#14467=AXIS2_PLACEMENT_3D('',#23534,#17351,#17352);
#14468=AXIS2_PLACEMENT_3D('',#23535,#17353,#17354);
#14469=AXIS2_PLACEMENT_3D('',#23536,#17355,#17356);
#14470=AXIS2_PLACEMENT_3D('',#23537,#17357,#17358);
#14471=AXIS2_PLACEMENT_3D('',#23540,#17360,#17361);
#14472=AXIS2_PLACEMENT_3D('',#23541,#17362,#17363);
#17248=DIRECTION('axis',(0.,0.,1.));
#17249=DIRECTION('refdir',(1.,0.,0.));
#17250=DIRECTION('center_axis',(1.,0.,0.));
#17251=DIRECTION('ref_axis',(0.,0.207879895528894,-0.978154358490978));
#17252=DIRECTION('',(-1.,0.,0.));
#17253=DIRECTION('center_axis',(1.,0.,0.));
#17254=DIRECTION('ref_axis',(0.,0.,-1.));
#17255=DIRECTION('center_axis',(1.,0.,0.));
#17256=DIRECTION('ref_axis',(0.,0.,-1.));
#17257=DIRECTION('',(-1.,0.,0.));
#17258=DIRECTION('center_axis',(1.,0.,0.));
#17259=DIRECTION('ref_axis',(0.,0.,-1.));
#17260=DIRECTION('',(-1.,0.,0.));
#17261=DIRECTION('center_axis',(1.,0.,0.));
#17262=DIRECTION('ref_axis',(0.,0.,-1.));
#17263=DIRECTION('',(-1.,0.,0.));
#17264=DIRECTION('center_axis',(1.,0.,0.));
#17265=DIRECTION('ref_axis',(0.,0.,-1.));
#17266=DIRECTION('',(-1.,0.,0.));
#17267=DIRECTION('center_axis',(1.,0.,0.));
#17268=DIRECTION('ref_axis',(0.,0.,-1.));
#17269=DIRECTION('',(-1.,0.,0.));
#17270=DIRECTION('center_axis',(1.,0.,0.));
#17271=DIRECTION('ref_axis',(0.,0.,-1.));
#17272=DIRECTION('',(-1.,0.,0.));
#17273=DIRECTION('center_axis',(1.,0.,0.));
#17274=DIRECTION('ref_axis',(0.,0.,-1.));
#17275=DIRECTION('',(-1.,0.,0.));
#17276=DIRECTION('center_axis',(1.,0.,0.));
#17277=DIRECTION('ref_axis',(0.,0.,-1.));
#17278=DIRECTION('',(-1.,0.,0.));
#17279=DIRECTION('center_axis',(1.,0.,0.));
#17280=DIRECTION('ref_axis',(0.,0.,-1.));
#17281=DIRECTION('center_axis',(1.,0.,0.));
#17282=DIRECTION('ref_axis',(0.,2.68771689099506E-14,-1.));
#17283=DIRECTION('',(1.,3.30650148539799E-30,-1.22464679914735E-16));
#17284=DIRECTION('center_axis',(-1.,0.,0.));
#17285=DIRECTION('ref_axis',(0.,2.68771689099506E-14,-1.));
#17286=DIRECTION('center_axis',(1.,0.,0.));
#17287=DIRECTION('ref_axis',(0.,2.68771689099506E-14,-1.));
#17288=DIRECTION('',(1.,3.30650148539799E-30,-1.22464679914735E-16));
#17289=DIRECTION('center_axis',(1.,0.,0.));
#17290=DIRECTION('ref_axis',(0.,2.68771689099506E-14,-1.));
#17291=DIRECTION('',(1.,3.30650148539799E-30,-1.22464679914735E-16));
#17292=DIRECTION('center_axis',(1.,0.,0.));
#17293=DIRECTION('ref_axis',(0.,2.68771689099506E-14,-1.));
#17294=DIRECTION('',(1.,3.30650148539799E-30,-1.22464679914735E-16));
#17295=DIRECTION('center_axis',(1.,0.,0.));
#17296=DIRECTION('ref_axis',(0.,2.68771689099506E-14,-1.));
#17297=DIRECTION('',(1.,3.30650148539799E-30,-1.22464679914735E-16));
#17298=DIRECTION('center_axis',(1.,0.,0.));
#17299=DIRECTION('ref_axis',(0.,2.68771689099506E-14,-1.));
#17300=DIRECTION('',(1.,3.30650148539799E-30,-1.22464679914735E-16));
#17301=DIRECTION('center_axis',(1.,0.,0.));
#17302=DIRECTION('ref_axis',(0.,2.68771689099506E-14,-1.));
#17303=DIRECTION('',(1.,3.30650148539799E-30,-1.22464679914735E-16));
#17304=DIRECTION('center_axis',(1.,0.,0.));
#17305=DIRECTION('ref_axis',(0.,2.68771689099506E-14,-1.));
#17306=DIRECTION('',(1.,3.30650148539799E-30,-1.22464679914735E-16));
#17307=DIRECTION('center_axis',(1.,0.,0.));
#17308=DIRECTION('ref_axis',(0.,2.68771689099506E-14,-1.));
#17309=DIRECTION('',(1.,3.30650148539799E-30,-1.22464679914735E-16));
#17310=DIRECTION('center_axis',(1.,0.,0.));
#17311=DIRECTION('ref_axis',(0.,2.68771689099506E-14,-1.));
#17312=DIRECTION('center_axis',(1.,0.,0.));
#17313=DIRECTION('ref_axis',(0.,2.68771689099506E-14,-1.));
#17314=DIRECTION('center_axis',(1.,0.,0.));
#17315=DIRECTION('ref_axis',(0.,0.,-1.));
#17316=DIRECTION('',(0.,1.,0.));
#17317=DIRECTION('center_axis',(1.,0.,0.));
#17318=DIRECTION('ref_axis',(0.,0.,-1.));
#17319=DIRECTION('center_axis',(1.,0.,0.));
#17320=DIRECTION('ref_axis',(0.,0.,-1.));
#17321=DIRECTION('center_axis',(-1.,0.,0.));
#17322=DIRECTION('ref_axis',(0.,0.,-1.));
#17323=DIRECTION('center_axis',(-1.,0.,0.));
#17324=DIRECTION('ref_axis',(0.,0.,-1.));
#17325=DIRECTION('center_axis',(-1.,0.,0.));
#17326=DIRECTION('ref_axis',(0.,0.,-1.));
#17327=DIRECTION('center_axis',(1.,0.,0.));
#17328=DIRECTION('ref_axis',(0.,0.,-1.));
#17329=DIRECTION('center_axis',(1.,0.,0.));
#17330=DIRECTION('ref_axis',(0.,0.,-1.));
#17331=DIRECTION('',(1.,0.,0.));
#17332=DIRECTION('center_axis',(1.,0.,0.));
#17333=DIRECTION('ref_axis',(0.,0.,-1.));
#17334=DIRECTION('center_axis',(1.,0.,0.));
#17335=DIRECTION('ref_axis',(0.,0.,-1.));
#17336=DIRECTION('',(1.,0.,0.));
#17337=DIRECTION('center_axis',(1.,0.,0.));
#17338=DIRECTION('ref_axis',(0.,0.,-1.));
#17339=DIRECTION('center_axis',(1.,0.,0.));
#17340=DIRECTION('ref_axis',(0.,0.,-1.));
#17341=DIRECTION('',(1.,0.,0.));
#17342=DIRECTION('center_axis',(0.,0.,1.));
#17343=DIRECTION('ref_axis',(0.,-1.,0.));
#17344=DIRECTION('',(0.,-1.,0.));
#17345=DIRECTION('',(-1.,0.,0.));
#17346=DIRECTION('',(1.,0.,0.));
#17347=DIRECTION('center_axis',(1.,0.,0.));
#17348=DIRECTION('ref_axis',(0.,0.,-1.));
#17349=DIRECTION('center_axis',(1.,0.,0.));
#17350=DIRECTION('ref_axis',(0.,0.,-1.));
#17351=DIRECTION('center_axis',(1.,0.,0.));
#17352=DIRECTION('ref_axis',(0.,0.,-1.));
#17353=DIRECTION('center_axis',(1.,0.,0.));
#17354=DIRECTION('ref_axis',(0.,-1.22464679914735E-16,1.));
#17355=DIRECTION('center_axis',(1.,0.,0.));
#17356=DIRECTION('ref_axis',(0.,0.,-1.));
#17357=DIRECTION('center_axis',(1.,0.,0.));
#17358=DIRECTION('ref_axis',(0.,0.,-1.));
#17359=DIRECTION('',(-1.,0.,0.));
#17360=DIRECTION('center_axis',(1.,0.,0.));
#17361=DIRECTION('ref_axis',(0.,0.,-1.));
#17362=DIRECTION('center_axis',(1.,0.,0.));
#17363=DIRECTION('ref_axis',(0.,0.,-1.));
#21341=CARTESIAN_POINT('',(0.,0.,0.));
#21342=CARTESIAN_POINT('Origin',(12.5,0.,4.));
#21343=CARTESIAN_POINT('',(12.7800042915148,-1.13874042544416E-5,4.45787212683272));
#21344=CARTESIAN_POINT('',(12.6699957084852,1.09516003635735E-5,4.45788309353564));
#21345=CARTESIAN_POINT('',(12.5,-5.60735153159594E-17,4.457875));
#21346=CARTESIAN_POINT('',(12.5,-0.186196943290586,3.58169363627331));
#21347=CARTESIAN_POINT('Ctrl Pts',(12.6699957084852,1.09516003635735E-5,
4.45788309353564));
#21348=CARTESIAN_POINT('Ctrl Pts',(12.6684300766731,0.0150239422001319,
4.45789815019349));
#21349=CARTESIAN_POINT('Ctrl Pts',(12.6668644448611,0.0300354905662504,
4.45717403092565));
#21350=CARTESIAN_POINT('Ctrl Pts',(12.6652988130491,0.0449730203321769,
4.45569984746698));
#21351=CARTESIAN_POINT('Ctrl Pts',(12.6574274409991,0.120072959788606,4.44828824124903));
#21352=CARTESIAN_POINT('Ctrl Pts',(12.6495560689492,0.193301947984492,4.42191743369942));
#21353=CARTESIAN_POINT('Ctrl Pts',(12.6416846968992,0.255884660534875,4.37974732787395));
#21354=CARTESIAN_POINT('Ctrl Pts',(12.6338133248492,0.318467373085258,4.33757722204849));
#21355=CARTESIAN_POINT('Ctrl Pts',(12.6259419527993,0.370403809990138,4.27960781794716));
#21356=CARTESIAN_POINT('Ctrl Pts',(12.6180705807493,0.405471379329245,4.2127856577826));
#21357=CARTESIAN_POINT('Ctrl Pts',(12.6101992086994,0.440538948668352,4.14596349761803));
#21358=CARTESIAN_POINT('Ctrl Pts',(12.6023278366494,0.458737650441686,4.07028858139023));
#21359=CARTESIAN_POINT('Ctrl Pts',(12.5944564645995,0.457884906392306,3.99482861029462));
#21360=CARTESIAN_POINT('Ctrl Pts',(12.5865850925495,0.457032162342926,3.91936863919901));
#21361=CARTESIAN_POINT('Ctrl Pts',(12.5787137204996,0.437127972470831,3.84412361323559));
#21362=CARTESIAN_POINT('Ctrl Pts',(12.5708423484496,0.400561475243013,3.77811083326841));
#21363=CARTESIAN_POINT('Ctrl Pts',(12.5629709763996,0.363994978015195,3.71209805330123));
#21364=CARTESIAN_POINT('Ctrl Pts',(12.5550996043497,0.310766173431653,3.6553175193303));
#21365=CARTESIAN_POINT('Ctrl Pts',(12.5472282322997,0.247245050961511,3.61457214242492));
#21366=CARTESIAN_POINT('Ctrl Pts',(12.5393568602498,0.183723928491369,3.57382676551955));
#21367=CARTESIAN_POINT('Ctrl Pts',(12.5314854881998,0.109910488134627,3.54911654567973));
#21368=CARTESIAN_POINT('Ctrl Pts',(12.5236141161499,0.034670519197381,3.5434092666393));
#21369=CARTESIAN_POINT('Ctrl Pts',(12.5157427440999,-0.0405694497398647,
3.53770198759887));
#21370=CARTESIAN_POINT('Ctrl Pts',(12.50787137205,-0.117235947257613,3.55099764935784));
#21371=CARTESIAN_POINT('Ctrl Pts',(12.5,-0.186196943290592,3.58169363627332));
#21372=CARTESIAN_POINT('',(12.5,-0.186217277007329,4.41832740439831));
#21373=CARTESIAN_POINT('Origin',(12.5,0.,4.));
#21374=CARTESIAN_POINT('Ctrl Pts',(12.5,-0.186217277007329,4.41832740439831));
#21375=CARTESIAN_POINT('Ctrl Pts',(12.5008157411716,-0.193365324225124,
4.41515241707318));
#21376=CARTESIAN_POINT('Ctrl Pts',(12.5016314823431,-0.200430783441492,
4.4117927098014));
#21377=CARTESIAN_POINT('Ctrl Pts',(12.5024472235147,-0.207403505574881,
4.40825058102053));
#21378=CARTESIAN_POINT('Ctrl Pts',(12.5103185955646,-0.274685741688951,
4.37407134077235));
#21379=CARTESIAN_POINT('Ctrl Pts',(12.5181899676146,-0.333333232193243,
4.32290684204764));
#21380=CARTESIAN_POINT('Ctrl Pts',(12.5260613396645,-0.376326743005614,
4.26088786252735));
#21381=CARTESIAN_POINT('Ctrl Pts',(12.5339327117145,-0.419320253817985,
4.19886888300706));
#21382=CARTESIAN_POINT('Ctrl Pts',(12.5418040837645,-0.446659784938435,
4.12599542269119));
#21383=CARTESIAN_POINT('Ctrl Pts',(12.5496754558144,-0.455065168373522,
4.05100019606997));
#21384=CARTESIAN_POINT('Ctrl Pts',(12.5575468278644,-0.463470551808608,
3.97600496944875));
#21385=CARTESIAN_POINT('Ctrl Pts',(12.5654181999143,-0.452941787558331,
3.89888797652218));
#21386=CARTESIAN_POINT('Ctrl Pts',(12.5732895719643,-0.424742400952558,
3.82888990513641));
#21387=CARTESIAN_POINT('Ctrl Pts',(12.5811609440142,-0.396543014346786,
3.75889183375065));
#21388=CARTESIAN_POINT('Ctrl Pts',(12.5890323160642,-0.350673005385519,
3.69601268390568));
#21389=CARTESIAN_POINT('Ctrl Pts',(12.5969036881141,-0.292628022669152,
3.64778723809593));
#21390=CARTESIAN_POINT('Ctrl Pts',(12.6047750601641,-0.234583039952784,
3.59956179228618));
#21391=CARTESIAN_POINT('Ctrl Pts',(12.6126464322141,-0.164363083481316,
3.56599005051166));
#21392=CARTESIAN_POINT('Ctrl Pts',(12.620517804264,-0.0903829156297007,
3.55109483330951));
#21393=CARTESIAN_POINT('Ctrl Pts',(12.628389176314,-0.0164027477780855,
3.53619961610736));
#21394=CARTESIAN_POINT('Ctrl Pts',(12.6362605483639,0.0613376314536766,
3.53998092347757));
#21395=CARTESIAN_POINT('Ctrl Pts',(12.6441319204139,0.13352290298843,3.56198566164487));
#21396=CARTESIAN_POINT('Ctrl Pts',(12.6520032924638,0.205708174523184,3.58399039981218));
#21397=CARTESIAN_POINT('Ctrl Pts',(12.6598746645138,0.272338338360929,3.62421856877658));
#21398=CARTESIAN_POINT('Ctrl Pts',(12.6677460365637,0.325429113408527,3.67784968145944));
#21399=CARTESIAN_POINT('Ctrl Pts',(12.6756174086137,0.378519888456125,3.7314807941423));
#21400=CARTESIAN_POINT('Ctrl Pts',(12.6834887806637,0.418071274713577,3.79851485054363));
#21401=CARTESIAN_POINT('Ctrl Pts',(12.6913601527136,0.439343931585728,3.87091926467948));
#21402=CARTESIAN_POINT('Ctrl Pts',(12.6992315247636,0.460616588457879,3.94332367881533));
#21403=CARTESIAN_POINT('Ctrl Pts',(12.7071028968135,0.46361051594473,4.02109845068571));
#21404=CARTESIAN_POINT('Ctrl Pts',(12.7149742688635,0.447966936692366,4.09492394607626));
#21405=CARTESIAN_POINT('Ctrl Pts',(12.7228456409134,0.432323357440003,4.16874944146681));
#21406=CARTESIAN_POINT('Ctrl Pts',(12.7307170129634,0.398042271448426,4.23862566037754));
#21407=CARTESIAN_POINT('Ctrl Pts',(12.7385883850133,0.349231538304918,4.29617944234672));
#21408=CARTESIAN_POINT('Ctrl Pts',(12.7464597570633,0.300420805161409,4.35373322431589));
#21409=CARTESIAN_POINT('Ctrl Pts',(12.7543311291133,0.237080424865968,4.39896456934351));
#21410=CARTESIAN_POINT('Ctrl Pts',(12.7622025011632,0.166800374688878,4.42645347375649));
#21411=CARTESIAN_POINT('Ctrl Pts',(12.7681364312804,0.113818899065861,4.4471763206439));
#21412=CARTESIAN_POINT('Ctrl Pts',(12.7740703613976,0.056893551674301,4.45781599184163));
#21413=CARTESIAN_POINT('Ctrl Pts',(12.7800042915148,-1.13874042544416E-5,
4.45787212683272));
#21414=CARTESIAN_POINT('Origin',(12.5,0.,4.));
#21415=CARTESIAN_POINT('',(13.0800042915148,2.8196954984682E-6,4.45783894202495));
#21416=CARTESIAN_POINT('',(12.9699957084852,-6.90274666573233E-6,4.45790451736119));
#21417=CARTESIAN_POINT('',(12.5,-5.60735153159594E-17,4.457875));
#21418=CARTESIAN_POINT('Ctrl Pts',(12.9699957084852,-6.90274666573233E-6,
4.45790451736119));
#21419=CARTESIAN_POINT('Ctrl Pts',(12.9628865412726,0.0681543496286777,
4.45785453236543));
#21420=CARTESIAN_POINT('Ctrl Pts',(12.95577737406,0.136337475731944,4.44242789501186));
#21421=CARTESIAN_POINT('Ctrl Pts',(12.9486682068475,0.197807532932104,4.41298560914613));
#21422=CARTESIAN_POINT('Ctrl Pts',(12.9407968347975,0.265868063186489,4.38038668734267));
#21423=CARTESIAN_POINT('Ctrl Pts',(12.9329254627476,0.325698883531032,4.33060565060516));
#21424=CARTESIAN_POINT('Ctrl Pts',(12.9250540906976,0.370130557623211,4.26960768492436));
#21425=CARTESIAN_POINT('Ctrl Pts',(12.9171827186476,0.41456223171539,4.20860971924356));
#21426=CARTESIAN_POINT('Ctrl Pts',(12.9093113465977,0.443594759555206,4.13639482461947));
#21427=CARTESIAN_POINT('Ctrl Pts',(12.9014399745477,0.453749217534713,4.06161640217293));
#21428=CARTESIAN_POINT('Ctrl Pts',(12.8935686024978,0.463903675514219,3.9868379797264));
#21429=CARTESIAN_POINT('Ctrl Pts',(12.8856972304478,0.455180063633418,3.90949602945742));
#21430=CARTESIAN_POINT('Ctrl Pts',(12.8778258583979,0.428623718850503,3.83885831972366));
#21431=CARTESIAN_POINT('Ctrl Pts',(12.8699544863479,0.402067374067587,3.7682206099899));
#21432=CARTESIAN_POINT('Ctrl Pts',(12.862083114298,0.357678296382559,3.70428714079136));
#21433=CARTESIAN_POINT('Ctrl Pts',(12.854211742248,0.300775561959983,3.65471896268111));
#21434=CARTESIAN_POINT('Ctrl Pts',(12.846340370198,0.243872827537407,3.60515078457087));
#21435=CARTESIAN_POINT('Ctrl Pts',(12.8384689981481,0.174456436377283,3.56994789754891));
#21436=CARTESIAN_POINT('Ctrl Pts',(12.8305976260981,0.100844448250471,3.55332860992135));
#21437=CARTESIAN_POINT('Ctrl Pts',(12.8227262540482,0.0272324601236582,
3.53670932229378));
#21438=CARTESIAN_POINT('Ctrl Pts',(12.8148548819982,-0.0505751249698428,
3.53867363406062));
#21439=CARTESIAN_POINT('Ctrl Pts',(12.8069835099483,-0.123254740362562,
3.558986165072));
#21440=CARTESIAN_POINT('Ctrl Pts',(12.7991121378983,-0.195934355755281,
3.57929869608338));
#21441=CARTESIAN_POINT('Ctrl Pts',(12.7912407658484,-0.263486001447217,
3.6179594463393));
#21442=CARTESIAN_POINT('Ctrl Pts',(12.7833693937984,-0.317815070570116,
3.67033575613656));
#21443=CARTESIAN_POINT('Ctrl Pts',(12.7754980217484,-0.372144139693014,
3.72271206593382));
#21444=CARTESIAN_POINT('Ctrl Pts',(12.7676266496985,-0.413250632246875,
3.78880393527241));
#21445=CARTESIAN_POINT('Ctrl Pts',(12.7597552776485,-0.43620881068128,3.86069167744737));
#21446=CARTESIAN_POINT('Ctrl Pts',(12.7518839055986,-0.459166989115684,
3.93257941962233));
#21447=CARTESIAN_POINT('Ctrl Pts',(12.7440125335486,-0.463976853430633,
4.01026303463365));
#21448=CARTESIAN_POINT('Ctrl Pts',(12.7361411614987,-0.450062064178823,
4.08443380953254));
#21449=CARTESIAN_POINT('Ctrl Pts',(12.7282697894487,-0.436147274927012,
4.15860458443143));
#21450=CARTESIAN_POINT('Ctrl Pts',(12.7203984173988,-0.403507832108441,
4.22926251921788));
#21451=CARTESIAN_POINT('Ctrl Pts',(12.7125270453488,-0.356054829243877,
4.28794078818664));
#21452=CARTESIAN_POINT('Ctrl Pts',(12.7046556732988,-0.308601826379312,
4.3466190571554));
#21453=CARTESIAN_POINT('Ctrl Pts',(12.6967843012489,-0.246335263468753,
4.39331766030646));
#21454=CARTESIAN_POINT('Ctrl Pts',(12.6889129291989,-0.176716536654988,
4.42244075943884));
#21455=CARTESIAN_POINT('Ctrl Pts',(12.682607188961,-0.120945115332726,4.44577121528397));
#21456=CARTESIAN_POINT('Ctrl Pts',(12.6763014487231,-0.0604553842193124,
4.45782245132557));
#21457=CARTESIAN_POINT('Ctrl Pts',(12.6699957084852,1.09516003635735E-5,
4.45788309353564));
#21458=CARTESIAN_POINT('Ctrl Pts',(12.7800042915148,-1.13874042544416E-5,
4.45787212683272));
#21459=CARTESIAN_POINT('Ctrl Pts',(12.7819417334476,-0.0185909818676029,
4.45789045503738));
#21460=CARTESIAN_POINT('Ctrl Pts',(12.7838791753803,-0.0371684007279871,
4.45678053845584));
#21461=CARTESIAN_POINT('Ctrl Pts',(12.7858166173131,-0.0556056617636943,
4.45452496135198));
#21462=CARTESIAN_POINT('Ctrl Pts',(12.793687989363,-0.130511927980435,4.44536108073615));
#21463=CARTESIAN_POINT('Ctrl Pts',(12.801559361413,-0.203104740355178,4.41728685570614));
#21464=CARTESIAN_POINT('Ctrl Pts',(12.8094307334629,-0.264685413403174,
4.37366637792357));
#21465=CARTESIAN_POINT('Ctrl Pts',(12.8173021055129,-0.32626608645117,4.33004590014099));
#21466=CARTESIAN_POINT('Ctrl Pts',(12.8251734775629,-0.37683462017242,4.27087916960585));
#21467=CARTESIAN_POINT('Ctrl Pts',(12.8330448496128,-0.410331463567461,
4.20325604577686));
#21468=CARTESIAN_POINT('Ctrl Pts',(12.8409162216628,-0.443828306962503,
4.13563292194788));
#21469=CARTESIAN_POINT('Ctrl Pts',(12.8487875937127,-0.460253460031337,
4.05955340482505));
#21470=CARTESIAN_POINT('Ctrl Pts',(12.8566589657627,-0.457638721839564,
3.98413398734005));
#21471=CARTESIAN_POINT('Ctrl Pts',(12.8645303378126,-0.45502398364779,3.90871456985506));
#21472=CARTESIAN_POINT('Ctrl Pts',(12.8724017098626,-0.433369354195409,
3.8339552520079));
#21473=CARTESIAN_POINT('Ctrl Pts',(12.8802730819125,-0.395269674734573,
3.76881432927916));
#21474=CARTESIAN_POINT('Ctrl Pts',(12.8881444539625,-0.357169995273737,
3.70367340655041));
#21475=CARTESIAN_POINT('Ctrl Pts',(12.8960158260125,-0.302625265804445,
3.64815087894007));
#21476=CARTESIAN_POINT('Ctrl Pts',(12.9038871980624,-0.238171498431664,
3.6088999265713));
#21477=CARTESIAN_POINT('Ctrl Pts',(12.9117585701124,-0.173717731058884,
3.56964897420252));
#21478=CARTESIAN_POINT('Ctrl Pts',(12.9196299421623,-0.0993549257826154,
3.5466695970753));
#21479=CARTESIAN_POINT('Ctrl Pts',(12.9275013142123,-0.023993864556795,
3.54271537903906));
#21480=CARTESIAN_POINT('Ctrl Pts',(12.9353726862622,0.0513671966690251,
3.53876116100282));
#21481=CARTESIAN_POINT('Ctrl Pts',(12.9432440583122,0.127726513844396,3.55383210205756));
#21482=CARTESIAN_POINT('Ctrl Pts',(12.9511154303621,0.195934065997641,3.58612227423372));
#21483=CARTESIAN_POINT('Ctrl Pts',(12.9589868024121,0.264141618150887,3.61841244640988));
#21484=CARTESIAN_POINT('Ctrl Pts',(12.9668581744621,0.324197405282005,3.66792184970745));
#21485=CARTESIAN_POINT('Ctrl Pts',(12.974729546512,0.368905033668178,3.72871784755079));
#21486=CARTESIAN_POINT('Ctrl Pts',(12.982600918562,0.41361266205435,3.78951384539413));
#21487=CARTESIAN_POINT('Ctrl Pts',(12.9904722906119,0.442972131695578,3.86159643778324));
#21488=CARTESIAN_POINT('Ctrl Pts',(12.9983436626619,0.453465341949404,3.93632807718928));
#21489=CARTESIAN_POINT('Ctrl Pts',(13.0062150347118,0.46395855220323,4.01105971659532));
#21490=CARTESIAN_POINT('Ctrl Pts',(13.0140864067618,0.455585503069655,4.0884404030183));
#21491=CARTESIAN_POINT('Ctrl Pts',(13.0219577788117,0.429349524305901,4.15919772637108));
#21492=CARTESIAN_POINT('Ctrl Pts',(13.0298291508617,0.403113545542148,4.22995504972387));
#21493=CARTESIAN_POINT('Ctrl Pts',(13.0377005229117,0.359014637148215,4.29408901000646));
#21494=CARTESIAN_POINT('Ctrl Pts',(13.0455718949616,0.302337104315659,4.34391453219887));
#21495=CARTESIAN_POINT('Ctrl Pts',(13.0534432670116,0.245659571483104,4.39374005439127));
#21496=CARTESIAN_POINT('Ctrl Pts',(13.0613146390615,0.176403414211925,4.4292571384935));
#21497=CARTESIAN_POINT('Ctrl Pts',(13.0691860111115,0.102867492605122,4.44620982627979));
#21498=CARTESIAN_POINT('Ctrl Pts',(13.0727921045793,0.0691786509558273,
4.45397632191734));
#21499=CARTESIAN_POINT('Ctrl Pts',(13.076398198047,0.0345915681853763,4.45784650391406));
#21500=CARTESIAN_POINT('Ctrl Pts',(13.0800042915148,2.8196954984682E-6,
4.45783894202495));
#21501=CARTESIAN_POINT('Origin',(12.5,0.,4.));
#21502=CARTESIAN_POINT('',(13.3800042915148,1.00338821889499E-5,4.45789143379912));
#21503=CARTESIAN_POINT('',(13.2699957084852,-6.83105689078257E-6,4.45784477598907));
#21504=CARTESIAN_POINT('',(12.5,-5.60735153159594E-17,4.457875));
#21505=CARTESIAN_POINT('Ctrl Pts',(13.2699957084852,-6.83105689078257E-6,
4.45784477598907));
#21506=CARTESIAN_POINT('Ctrl Pts',(13.265214377922,0.0458528260712244,4.45782008288951));
#21507=CARTESIAN_POINT('Ctrl Pts',(13.2604330473589,0.091719698604501,4.45096974854549));
#21508=CARTESIAN_POINT('Ctrl Pts',(13.2556517167957,0.135506404234727,4.43740478719402));
#21509=CARTESIAN_POINT('Ctrl Pts',(13.2477803447458,0.207591244700251,4.41507316710824));
#21510=CARTESIAN_POINT('Ctrl Pts',(13.2399089726958,0.274038390871736,4.37454348113122));
#21511=CARTESIAN_POINT('Ctrl Pts',(13.2320376006459,0.326885582178656,4.32067233995558));
#21512=CARTESIAN_POINT('Ctrl Pts',(13.2241662285959,0.379732773485576,4.26680119877995));
#21513=CARTESIAN_POINT('Ctrl Pts',(13.2162948565459,0.418980009927931,4.19958860240569));
#21514=CARTESIAN_POINT('Ctrl Pts',(13.208423484496,0.439924354792367,4.12708853413817));
#21515=CARTESIAN_POINT('Ctrl Pts',(13.200552112446,0.460868699656804,4.05458846587065));
#21516=CARTESIAN_POINT('Ctrl Pts',(13.1926807403961,0.463510152943321,3.97680092570987));
#21517=CARTESIAN_POINT('Ctrl Pts',(13.1848093683461,0.447532193317848,3.90304707640827));
#21518=CARTESIAN_POINT('Ctrl Pts',(13.1769379962962,0.431554233692375,3.82929322710668));
#21519=CARTESIAN_POINT('Ctrl Pts',(13.1690666242462,0.396956861154912,3.75957306866428));
#21520=CARTESIAN_POINT('Ctrl Pts',(13.1611952521963,0.347885826291745,3.70224106173923));
#21521=CARTESIAN_POINT('Ctrl Pts',(13.1533238801463,0.298814791428577,3.64490905481418));
#21522=CARTESIAN_POINT('Ctrl Pts',(13.1454525080963,0.235270094239705,3.59996519940648));
#21523=CARTESIAN_POINT('Ctrl Pts',(13.1375811360464,0.164866199243897,3.57279504942506));
#21524=CARTESIAN_POINT('Ctrl Pts',(13.1297097639964,0.0944623042480882,
3.54562489944363));
#21525=CARTESIAN_POINT('Ctrl Pts',(13.1218383919465,0.0171992114453437,
3.53622845488849));
#21526=CARTESIAN_POINT('Ctrl Pts',(13.1139670198965,-0.0576647601420857,
3.54573167743434));
#21527=CARTESIAN_POINT('Ctrl Pts',(13.1060956478466,-0.132528731729515,
3.55523489998019));
#21528=CARTESIAN_POINT('Ctrl Pts',(13.0982242757966,-0.204993582101629,
3.58363778962703));
#21529=CARTESIAN_POINT('Ctrl Pts',(13.0903529037467,-0.266375958336211,
3.62753687126191));
#21530=CARTESIAN_POINT('Ctrl Pts',(13.0824815316967,-0.327758334570793,
3.67143595289679));
#21531=CARTESIAN_POINT('Ctrl Pts',(13.0746101596467,-0.378058236667844,
3.73083122651971));
#21532=CARTESIAN_POINT('Ctrl Pts',(13.0667387875968,-0.411248303781717,
3.79860544673343));
#21533=CARTESIAN_POINT('Ctrl Pts',(13.0588674155468,-0.444438370895591,
3.86637966694714));
#21534=CARTESIAN_POINT('Ctrl Pts',(13.0509960434969,-0.460518603026287,
3.94253283375165));
#21535=CARTESIAN_POINT('Ctrl Pts',(13.0431246714469,-0.457562130387816,
4.0179396288708));
#21536=CARTESIAN_POINT('Ctrl Pts',(13.035253299397,-0.454605657749345,4.09334642398995));
#21537=CARTESIAN_POINT('Ctrl Pts',(13.027381927347,-0.432612480341706,4.16800684742375));
#21538=CARTESIAN_POINT('Ctrl Pts',(13.0195105552971,-0.394218007200806,
4.23297445406563));
#21539=CARTESIAN_POINT('Ctrl Pts',(13.0116391832471,-0.355823534059905,
4.29794206070751));
#21540=CARTESIAN_POINT('Ctrl Pts',(13.0037678111972,-0.301027765185743,
4.35321685055749));
#21541=CARTESIAN_POINT('Ctrl Pts',(12.9958964391472,-0.236396794305188,
4.39217532952931));
#21542=CARTESIAN_POINT('Ctrl Pts',(12.9880250670972,-0.171765823424632,
4.43113380850113));
#21543=CARTESIAN_POINT('Ctrl Pts',(12.9801536950473,-0.0972996505376846,
4.45377597659478));
#21544=CARTESIAN_POINT('Ctrl Pts',(12.9722823229973,-0.0219214440120968,
4.4573886572069));
#21545=CARTESIAN_POINT('Ctrl Pts',(12.9715201181599,-0.014622381881285,
4.45773848219561));
#21546=CARTESIAN_POINT('Ctrl Pts',(12.9707579133226,-0.00731476803234869,
4.45790987647069));
#21547=CARTESIAN_POINT('Ctrl Pts',(12.9699957084852,-6.90274666573233E-6,
4.45790451736119));
#21548=CARTESIAN_POINT('Ctrl Pts',(13.0800042915148,2.8196954984682E-6,
4.45783894202495));
#21549=CARTESIAN_POINT('Ctrl Pts',(13.084269570097,-0.0409086678841046,
4.4578299978409));
#21550=CARTESIAN_POINT('Ctrl Pts',(13.0885348486792,-0.0818224858219862,
4.45239605085009));
#21551=CARTESIAN_POINT('Ctrl Pts',(13.0928001272613,-0.121255029803553,
4.44156782927524));
#21552=CARTESIAN_POINT('Ctrl Pts',(13.1006714993113,-0.194025944662995,
4.42158485301405));
#21553=CARTESIAN_POINT('Ctrl Pts',(13.1085428713613,-0.261752088439453,
4.3832306090213));
#21554=CARTESIAN_POINT('Ctrl Pts',(13.1164142434112,-0.31631794022257,4.33110102808186));
#21555=CARTESIAN_POINT('Ctrl Pts',(13.1242856154612,-0.370883792005687,
4.27897144714243));
#21556=CARTESIAN_POINT('Ctrl Pts',(13.1321569875111,-0.412289351795463,
4.21306652925631));
#21557=CARTESIAN_POINT('Ctrl Pts',(13.1400283595611,-0.435573054271055,
4.14128356060242));
#21558=CARTESIAN_POINT('Ctrl Pts',(13.147899731611,-0.458856756746647,4.06950059194853));
#21559=CARTESIAN_POINT('Ctrl Pts',(13.155771103661,-0.464018601908056,3.99183957252686));
#21560=CARTESIAN_POINT('Ctrl Pts',(13.1636424757109,-0.45044005369213,3.91760650430194));
#21561=CARTESIAN_POINT('Ctrl Pts',(13.1715138477609,-0.436861505476204,
3.84337343607703));
#21562=CARTESIAN_POINT('Ctrl Pts',(13.1793852198109,-0.404542563882944,
3.77256831904885));
#21563=CARTESIAN_POINT('Ctrl Pts',(13.1872565918608,-0.357355958580309,
3.7136756228145));
#21564=CARTESIAN_POINT('Ctrl Pts',(13.1951279639108,-0.310169353277673,
3.65478292658016));
#21565=CARTESIAN_POINT('Ctrl Pts',(13.2029993359607,-0.248115084265664,
3.60780265113964));
#21566=CARTESIAN_POINT('Ctrl Pts',(13.2108707080107,-0.178629020319019,
3.57836437152041));
#21567=CARTESIAN_POINT('Ctrl Pts',(13.2187420800606,-0.109142956372374,
3.54892609190117));
#21568=CARTESIAN_POINT('Ctrl Pts',(13.2266134521106,-0.0322250974910928,
3.53702980810322));
#21569=CARTESIAN_POINT('Ctrl Pts',(13.2344848241605,0.0429076061587562,
3.54410103373967));
#21570=CARTESIAN_POINT('Ctrl Pts',(13.2423561962105,0.118040309808605,3.55117225937612));
#21571=CARTESIAN_POINT('Ctrl Pts',(13.2502275682605,0.191387858227023,3.57721099444696));
#21572=CARTESIAN_POINT('Ctrl Pts',(13.2580989403104,0.254161126126225,3.61909705689013));
#21573=CARTESIAN_POINT('Ctrl Pts',(13.2659703123604,0.316934394025428,3.66098311933329));
#21574=CARTESIAN_POINT('Ctrl Pts',(13.2738416844103,0.369133381405416,3.71871650914877));
#21575=CARTESIAN_POINT('Ctrl Pts',(13.2817130564603,0.404503162915977,3.78537912195109));
#21576=CARTESIAN_POINT('Ctrl Pts',(13.2895844285102,0.43987294442654,3.85204173475342));
#21577=CARTESIAN_POINT('Ctrl Pts',(13.2974558005602,0.458413520067676,3.92763357054259));
#21578=CARTESIAN_POINT('Ctrl Pts',(13.3053271726101,0.457903200829578,4.00309657448501));
#21579=CARTESIAN_POINT('Ctrl Pts',(13.3131985446601,0.457392881591479,4.07855957842742));
#21580=CARTESIAN_POINT('Ctrl Pts',(13.3210699167101,0.437831667474148,4.15389375052308));
#21581=CARTESIAN_POINT('Ctrl Pts',(13.32894128876,0.401563549045306,4.22007191138728));
#21582=CARTESIAN_POINT('Ctrl Pts',(13.33681266081,0.365295430616463,4.28625007225149));
#21583=CARTESIAN_POINT('Ctrl Pts',(13.3446840328599,0.31232040787611,4.34327222188425));
#21584=CARTESIAN_POINT('Ctrl Pts',(13.3525554049099,0.248986397312635,4.38430548273058));
#21585=CARTESIAN_POINT('Ctrl Pts',(13.3604267769598,0.185652386749161,4.42533874357692));
#21586=CARTESIAN_POINT('Ctrl Pts',(13.3682981490098,0.111959388362564,4.45038311563682));
#21587=CARTESIAN_POINT('Ctrl Pts',(13.3761695210597,0.0367379221854645,
4.45643756985705));
#21588=CARTESIAN_POINT('Ctrl Pts',(13.3774477778781,0.024522472144774,4.45742077168506));
#21589=CARTESIAN_POINT('Ctrl Pts',(13.3787260346965,0.0122667140672706,
4.45790318029249));
#21590=CARTESIAN_POINT('Ctrl Pts',(13.3800042915148,1.00338821889499E-5,
4.45789143379912));
#21591=CARTESIAN_POINT('Origin',(12.5,0.,4.));
#21592=CARTESIAN_POINT('',(13.6800042915148,-8.85210990424201E-6,4.45789764648838));
#21593=CARTESIAN_POINT('',(13.5699957084852,1.03170790782398E-5,4.4578580083501));
#21594=CARTESIAN_POINT('',(12.5,-5.60735153159594E-17,4.457875));
#21595=CARTESIAN_POINT('Ctrl Pts',(13.5699957084852,1.03170790782398E-5,
4.4578580083501));
#21596=CARTESIAN_POINT('Ctrl Pts',(13.5675422145714,0.0235408097699949,
4.45787795556699));
#21597=CARTESIAN_POINT('Ctrl Pts',(13.5650887206577,0.0470683081483061,
4.45609516914004));
#21598=CARTESIAN_POINT('Ctrl Pts',(13.562635226744,0.0703115975725277,4.45248338388903));
#21599=CARTESIAN_POINT('Ctrl Pts',(13.554763854694,0.144881409096958,4.44089594716616));
#21600=CARTESIAN_POINT('Ctrl Pts',(13.5468924826441,0.21652593236894,4.41048310506186));
#21601=CARTESIAN_POINT('Ctrl Pts',(13.5390211105941,0.276660113016528,4.36488918223832));
#21602=CARTESIAN_POINT('Ctrl Pts',(13.5311497385442,0.336794293664116,4.31929525941478));
#21603=CARTESIAN_POINT('Ctrl Pts',(13.5232783664942,0.385418131687311,4.25852025587201));
#21604=CARTESIAN_POINT('Ctrl Pts',(13.5154069944443,0.416705106451492,4.18984674794718));
#21605=CARTESIAN_POINT('Ctrl Pts',(13.5075356223943,0.447992081215673,4.12117324002235));
#21606=CARTESIAN_POINT('Ctrl Pts',(13.4996642503443,0.461942192720839,4.04460122771548));
#21607=CARTESIAN_POINT('Ctrl Pts',(13.4917928782944,0.456883820300162,3.96930621892307));
#21608=CARTESIAN_POINT('Ctrl Pts',(13.4839215062444,0.451825447879485,3.89401121013066));
#21609=CARTESIAN_POINT('Ctrl Pts',(13.4760501341945,0.427758591532965,3.81999320485271));
#21610=CARTESIAN_POINT('Ctrl Pts',(13.4681787621445,0.387567146091087,3.75612166820384));
#21611=CARTESIAN_POINT('Ctrl Pts',(13.4603073900946,0.347375700649209,3.69225013155497));
#21612=CARTESIAN_POINT('Ctrl Pts',(13.4524360180446,0.291059666111973,3.63852506353517));
#21613=CARTESIAN_POINT('Ctrl Pts',(13.4445646459947,0.225367307335285,3.60138425741911));
#21614=CARTESIAN_POINT('Ctrl Pts',(13.4366932739447,0.159674948558598,3.56424345130305));
#21615=CARTESIAN_POINT('Ctrl Pts',(13.4288219018947,0.0846062655424597,
3.54368690709073));
#21616=CARTESIAN_POINT('Ctrl Pts',(13.4209505298448,0.00915662451852634,
3.54217788424291));
#21617=CARTESIAN_POINT('Ctrl Pts',(13.4130791577948,-0.0662930165054059,
3.54066886139509));
#21618=CARTESIAN_POINT('Ctrl Pts',(13.4052077857449,-0.142123615537132,
3.55820735991178));
#21619=CARTESIAN_POINT('Ctrl Pts',(13.3973364136949,-0.209248507106454,
3.5926917681625));
#21620=CARTESIAN_POINT('Ctrl Pts',(13.389465041645,-0.276373398675776,3.62717617641322));
#21621=CARTESIAN_POINT('Ctrl Pts',(13.381593669595,-0.334792582782693,3.67860649439798));
#21622=CARTESIAN_POINT('Ctrl Pts',(13.3737222975451,-0.377505777353741,
3.74081990525232));
#21623=CARTESIAN_POINT('Ctrl Pts',(13.3658509254951,-0.420218971924789,
3.80303331610666));
#21624=CARTESIAN_POINT('Ctrl Pts',(13.3579795534451,-0.44722617695997,3.87602981983059));
#21625=CARTESIAN_POINT('Ctrl Pts',(13.3501081813952,-0.455291160112798,
3.95106235628872));
#21626=CARTESIAN_POINT('Ctrl Pts',(13.3422368093452,-0.463356143265626,
4.02609489274685));
#21627=CARTESIAN_POINT('Ctrl Pts',(13.3343654372953,-0.452478904536101,
4.10316346193917));
#21628=CARTESIAN_POINT('Ctrl Pts',(13.3264940652453,-0.423962846915058,
4.17303305431203));
#21629=CARTESIAN_POINT('Ctrl Pts',(13.3186226931954,-0.395446789294015,
4.24290264668488));
#21630=CARTESIAN_POINT('Ctrl Pts',(13.3107513211454,-0.349291912781453,
4.30557326223827));
#21631=CARTESIAN_POINT('Ctrl Pts',(13.3028799490955,-0.291028886105345,
4.35353517632783));
#21632=CARTESIAN_POINT('Ctrl Pts',(13.2950085770455,-0.232765859429236,
4.4014970904174));
#21633=CARTESIAN_POINT('Ctrl Pts',(13.2871372049956,-0.162394682589579,
4.43475030304313));
#21634=CARTESIAN_POINT('Ctrl Pts',(13.2792658329456,-0.0883478267899694,
4.44931013225873));
#21635=CARTESIAN_POINT('Ctrl Pts',(13.2761757914588,-0.059279469337623,
4.4550258417985));
#21636=CARTESIAN_POINT('Ctrl Pts',(13.273085749972,-0.0296446570187532,
4.45786073445524));
#21637=CARTESIAN_POINT('Ctrl Pts',(13.2699957084852,-6.83105689078257E-6,
4.45784477598907));
#21638=CARTESIAN_POINT('Ctrl Pts',(13.3800042915148,1.00338821889499E-5,
4.45789143379912));
#21639=CARTESIAN_POINT('Ctrl Pts',(13.3865974067464,-0.0632086430349686,
4.45783084661254));
#21640=CARTESIAN_POINT('Ctrl Pts',(13.393190521978,-0.12645185159805,4.44462381290384));
#21641=CARTESIAN_POINT('Ctrl Pts',(13.3997836372096,-0.184315051738561,
4.41918121595096));
#21642=CARTESIAN_POINT('Ctrl Pts',(13.4076550092596,-0.253396625517876,
4.3888058714441));
#21643=CARTESIAN_POINT('Ctrl Pts',(13.4155263813095,-0.314809839108902,
4.34099064604983));
#21644=CARTESIAN_POINT('Ctrl Pts',(13.4233977533595,-0.361195640434018,
4.28146516557999));
#21645=CARTESIAN_POINT('Ctrl Pts',(13.4312691254094,-0.407581441759134,
4.22193968511016));
#21646=CARTESIAN_POINT('Ctrl Pts',(13.4391404974594,-0.438939830818339,
4.15070394956476));
#21647=CARTESIAN_POINT('Ctrl Pts',(13.4470118695093,-0.451513179494438,
4.07629402890356));
#21648=CARTESIAN_POINT('Ctrl Pts',(13.4548832415593,-0.464086528170537,
4.00188410824235));
#21649=CARTESIAN_POINT('Ctrl Pts',(13.4627546136093,-0.457874836463529,
3.92430000246534));
#21650=CARTESIAN_POINT('Ctrl Pts',(13.4706259856592,-0.433622441953051,
3.85283849709185));
#21651=CARTESIAN_POINT('Ctrl Pts',(13.4784973577092,-0.409370047442573,
3.78137699171835));
#21652=CARTESIAN_POINT('Ctrl Pts',(13.4863687297591,-0.367076950128625,
3.71603808674838));
#21653=CARTESIAN_POINT('Ctrl Pts',(13.4942401018091,-0.311811067605128,
3.66465124389307));
#21654=CARTESIAN_POINT('Ctrl Pts',(13.502111473859,-0.25654518508163,3.61326440103776));
#21655=CARTESIAN_POINT('Ctrl Pts',(13.509982845909,-0.188306517348584,3.5758296202971));
#21656=CARTESIAN_POINT('Ctrl Pts',(13.5178542179589,-0.115272000283325,
3.55683265457144));
#21657=CARTESIAN_POINT('Ctrl Pts',(13.5257255900089,-0.0422374832180674,
3.53783568884578));
#21658=CARTESIAN_POINT('Ctrl Pts',(13.5335969620589,0.035592883179403,3.53727653813511));
#21659=CARTESIAN_POINT('Ctrl Pts',(13.5414683341088,0.108892804353757,3.55522220461956));
#21660=CARTESIAN_POINT('Ctrl Pts',(13.5493397061588,0.182192725528112,3.573167871104));
#21661=CARTESIAN_POINT('Ctrl Pts',(13.5572110782087,0.250962201479351,3.60961835478357));
#21662=CARTESIAN_POINT('Ctrl Pts',(13.5650824502587,0.306960690387823,3.66020584957927));
#21663=CARTESIAN_POINT('Ctrl Pts',(13.5729538223086,0.362959179296295,3.71079334437498));
#21664=CARTESIAN_POINT('Ctrl Pts',(13.5808251943586,0.406186681162,3.77551785028682));
#21665=CARTESIAN_POINT('Ctrl Pts',(13.5886965664085,0.431463310113251,3.84662352810933));
#21666=CARTESIAN_POINT('Ctrl Pts',(13.5965679384585,0.456739939064502,3.91772920593184));
#21667=CARTESIAN_POINT('Ctrl Pts',(13.6044393105085,0.464065695101298,3.99521605566501));
#21668=CARTESIAN_POINT('Ctrl Pts',(13.6123106825584,0.452562744007997,4.06979894583348));
#21669=CARTESIAN_POINT('Ctrl Pts',(13.6201820546084,0.441059792914696,4.14438183600196));
#21670=CARTESIAN_POINT('Ctrl Pts',(13.6280534266583,0.410728134691299,4.21606076660573));
#21671=CARTESIAN_POINT('Ctrl Pts',(13.6359247987083,0.365202365858889,4.27624656029457));
#21672=CARTESIAN_POINT('Ctrl Pts',(13.6437961707582,0.319676597026479,4.33643235398341));
#21673=CARTESIAN_POINT('Ctrl Pts',(13.6516675428082,0.258956717585058,4.38512501075732));
#21674=CARTESIAN_POINT('Ctrl Pts',(13.6595389148581,0.190318698434502,4.41648976353532));
#21675=CARTESIAN_POINT('Ctrl Pts',(13.666360707077,0.130832969391341,4.44367229602021));
#21676=CARTESIAN_POINT('Ctrl Pts',(13.6731824992959,0.065399948454096,4.45783988979956));
#21677=CARTESIAN_POINT('Ctrl Pts',(13.6800042915148,-8.85210990424201E-6,
4.45789764648838));
#21678=CARTESIAN_POINT('Origin',(12.5,0.,4.));
#21679=CARTESIAN_POINT('',(13.9800042915148,-4.68615130337092E-6,4.45784092071359));
#21680=CARTESIAN_POINT('',(13.8699957084852,1.23414887176878E-6,4.4579133809027));
#21681=CARTESIAN_POINT('',(12.5,-5.60735153159594E-17,4.457875));
#21682=CARTESIAN_POINT('Ctrl Pts',(13.8699957084852,1.23414887176878E-6,
4.4579133809027));
#21683=CARTESIAN_POINT('Ctrl Pts',(13.8698700512209,0.00120594270822336,
4.45791357044259));
#21684=CARTESIAN_POINT('Ctrl Pts',(13.8697443939566,0.00241064979645091,
4.45790891401425));
#21685=CARTESIAN_POINT('Ctrl Pts',(13.8696187366923,0.00361531855258033,
4.45789940262096));
#21686=CARTESIAN_POINT('Ctrl Pts',(13.8617473646423,0.0790776965455978,
4.45730359373015));
#21687=CARTESIAN_POINT('Ctrl Pts',(13.8538759925924,0.154389660535011,4.43765704798318));
#21688=CARTESIAN_POINT('Ctrl Pts',(13.8460046205424,0.22052669229976,4.40131398110731));
#21689=CARTESIAN_POINT('Ctrl Pts',(13.8381332484924,0.286663724064511,4.36497091423144));
#21690=CARTESIAN_POINT('Ctrl Pts',(13.8302618764425,0.343625823604597,4.31193132622667));
#21691=CARTESIAN_POINT('Ctrl Pts',(13.8223905043925,0.384587309076409,4.24855087033892));
#21692=CARTESIAN_POINT('Ctrl Pts',(13.8145191323426,0.42554879454822,4.18517041445118));
#21693=CARTESIAN_POINT('Ctrl Pts',(13.8066477602926,0.450509665951756,4.11144909068046));
#21694=CARTESIAN_POINT('Ctrl Pts',(13.7987763882427,0.456478899990553,4.03622081324714));
#21695=CARTESIAN_POINT('Ctrl Pts',(13.7909050161927,0.46244813402935,3.96099253581381));
#21696=CARTESIAN_POINT('Ctrl Pts',(13.7830336441427,0.449425730703409,3.88425730471787));
#21697=CARTESIAN_POINT('Ctrl Pts',(13.7751622720928,0.418972144817937,3.81521018611534));
#21698=CARTESIAN_POINT('Ctrl Pts',(13.7672909000428,0.388518558932466,3.74616306751281));
#21699=CARTESIAN_POINT('Ctrl Pts',(13.7594195279929,0.340633790487464,3.68480406140369));
#21700=CARTESIAN_POINT('Ctrl Pts',(13.7515481559429,0.281055798532888,3.6384857242654));
#21701=CARTESIAN_POINT('Ctrl Pts',(13.743676783893,0.221477806578313,3.59216738712712));
#21702=CARTESIAN_POINT('Ctrl Pts',(13.735805411843,0.150206591114165,3.56088971895966));
#21703=CARTESIAN_POINT('Ctrl Pts',(13.7279340397931,0.0757824736049535,
3.54840067521841));
#21704=CARTESIAN_POINT('Ctrl Pts',(13.7200626677431,0.00135835609574232,
3.53591163147717));
#21705=CARTESIAN_POINT('Ctrl Pts',(13.7121912956931,-0.0762186634585312,
3.54221121216214));
#21706=CARTESIAN_POINT('Ctrl Pts',(13.7043199236432,-0.14765264866984,3.56654454809098));
#21707=CARTESIAN_POINT('Ctrl Pts',(13.6964485515932,-0.219086633881149,
3.59087788401983));
#21708=CARTESIAN_POINT('Ctrl Pts',(13.6885771795433,-0.284377584749494,
3.63324497519255));
#21709=CARTESIAN_POINT('Ctrl Pts',(13.6807058074933,-0.335701785830877,
3.68856903744356));
#21710=CARTESIAN_POINT('Ctrl Pts',(13.6728344354434,-0.38702598691226,3.74389309969457));
#21711=CARTESIAN_POINT('Ctrl Pts',(13.6649630633934,-0.424383438206683,
3.81217413302386));
#21712=CARTESIAN_POINT('Ctrl Pts',(13.6570916913435,-0.443297653083863,
3.88523012494906));
#21713=CARTESIAN_POINT('Ctrl Pts',(13.6492203192935,-0.462211867961044,
3.95828611687427));
#21714=CARTESIAN_POINT('Ctrl Pts',(13.6413489472436,-0.462682846420982,
4.03611706739538));
#21715=CARTESIAN_POINT('Ctrl Pts',(13.6334775751936,-0.444654151830396,
4.10939661196244));
#21716=CARTESIAN_POINT('Ctrl Pts',(13.6256062031436,-0.42662545723981,4.18267615652949));
#21717=CARTESIAN_POINT('Ctrl Pts',(13.6177348310937,-0.3900970895987,4.25140429514248));
#21718=CARTESIAN_POINT('Ctrl Pts',(13.6098634590437,-0.339446187702822,
4.3073454393722));
#21719=CARTESIAN_POINT('Ctrl Pts',(13.6019920869938,-0.288795285806945,
4.36328658360191));
#21720=CARTESIAN_POINT('Ctrl Pts',(13.5941207149438,-0.224021849656302,
4.40644073344835));
#21721=CARTESIAN_POINT('Ctrl Pts',(13.5862493428939,-0.152887581692542,
4.43163679270085));
#21722=CARTESIAN_POINT('Ctrl Pts',(13.5808314647576,-0.103925749791867,
4.44897928111035));
#21723=CARTESIAN_POINT('Ctrl Pts',(13.5754135866214,-0.0519504158054226,
4.45781396031326));
#21724=CARTESIAN_POINT('Ctrl Pts',(13.5699957084852,1.03170790782398E-5,
4.4578580083501));
#21725=CARTESIAN_POINT('Ctrl Pts',(13.6800042915148,-8.85210990424201E-6,
4.45789764648838));
#21726=CARTESIAN_POINT('Ctrl Pts',(13.6810538713459,-0.010072447664127,
4.45790653275371));
#21727=CARTESIAN_POINT('Ctrl Pts',(13.6821034511769,-0.0201354698749596,
4.45758141170421));
#21728=CARTESIAN_POINT('Ctrl Pts',(13.683153031008,-0.0301761699425476,
4.45691829561871));
#21729=CARTESIAN_POINT('Ctrl Pts',(13.691024403058,-0.105476860309351,4.45194522614199));
#21730=CARTESIAN_POINT('Ctrl Pts',(13.6988957751079,-0.179522082183268,
4.42796223840642));
#21731=CARTESIAN_POINT('Ctrl Pts',(13.7067671471579,-0.24343910912634,4.38784317739428));
#21732=CARTESIAN_POINT('Ctrl Pts',(13.7146385192078,-0.307356136069411,
4.34772411638213));
#21733=CARTESIAN_POINT('Ctrl Pts',(13.7225098912578,-0.361144968081636,
4.2914689820934));
#21734=CARTESIAN_POINT('Ctrl Pts',(13.7303812633077,-0.398360171146024,
4.22581874179975));
#21735=CARTESIAN_POINT('Ctrl Pts',(13.7382526353577,-0.435575374210412,
4.1601685015061));
#21736=CARTESIAN_POINT('Ctrl Pts',(13.7461240074077,-0.456216948326962,
4.08512315520753));
#21737=CARTESIAN_POINT('Ctrl Pts',(13.7539953794576,-0.457811445030669,
4.00967527273228));
#21738=CARTESIAN_POINT('Ctrl Pts',(13.7618667515076,-0.459405941734377,
3.93422739025703));
#21739=CARTESIAN_POINT('Ctrl Pts',(13.7697381235575,-0.441953361025241,
3.85837697160509));
#21740=CARTESIAN_POINT('Ctrl Pts',(13.7776094956075,-0.407545019133394,
3.79121305720166));
#21741=CARTESIAN_POINT('Ctrl Pts',(13.7854808676574,-0.373136677241547,
3.72404914279823));
#21742=CARTESIAN_POINT('Ctrl Pts',(13.7933522397074,-0.321772574166988,
3.6655717326433));
#21743=CARTESIAN_POINT('Ctrl Pts',(13.8012236117573,-0.259607592342073,
3.6227880859492));
#21744=CARTESIAN_POINT('Ctrl Pts',(13.8090949838073,-0.19744261051716,3.5800044392551));
#21745=CARTESIAN_POINT('Ctrl Pts',(13.8169663558573,-0.124476749941891,
3.55291455602183));
#21746=CARTESIAN_POINT('Ctrl Pts',(13.8248377279072,-0.0494533988297167,
3.54476457579874));
#21747=CARTESIAN_POINT('Ctrl Pts',(13.8327090999572,0.0255699522824598,
3.53661459557564));
#21748=CARTESIAN_POINT('Ctrl Pts',(13.8405804720071,0.102650793931542,3.54740451836272));
#21749=CARTESIAN_POINT('Ctrl Pts',(13.8484518440571,0.172552645974024,3.57584140410587));
#21750=CARTESIAN_POINT('Ctrl Pts',(13.856323216107,0.242454498016503,3.60427828984902));
#21751=CARTESIAN_POINT('Ctrl Pts',(13.864194588157,0.305177360452382,3.65036213854823));
#21752=CARTESIAN_POINT('Ctrl Pts',(13.8720659602069,0.353205247972751,3.70857079263049));
#21753=CARTESIAN_POINT('Ctrl Pts',(13.8799373322569,0.40123313549312,3.76677944671275));
#21754=CARTESIAN_POINT('Ctrl Pts',(13.8878087043068,0.434566048097978,3.83711290617806));
#21755=CARTESIAN_POINT('Ctrl Pts',(13.8956800763568,0.44920975351361,3.9111432194385));
#21756=CARTESIAN_POINT('Ctrl Pts',(13.9035514484068,0.463853458929242,3.98517353269893));
#21757=CARTESIAN_POINT('Ctrl Pts',(13.9114228204567,0.459807957155645,4.06290069975448));
#21758=CARTESIAN_POINT('Ctrl Pts',(13.9192941925067,0.437558014523894,4.13501079227018));
#21759=CARTESIAN_POINT('Ctrl Pts',(13.9271655645566,0.415308071892144,4.20712088478587));
#21760=CARTESIAN_POINT('Ctrl Pts',(13.9350369366066,0.374853688402242,4.27361390276169));
#21761=CARTESIAN_POINT('Ctrl Pts',(13.9429083086565,0.321042451364188,4.32652208887851));
#21762=CARTESIAN_POINT('Ctrl Pts',(13.9507796807065,0.267231214326134,4.37943027499533));
#21763=CARTESIAN_POINT('Ctrl Pts',(13.9586510527564,0.200063123739928,4.41875362925314));
#21764=CARTESIAN_POINT('Ctrl Pts',(13.9665224248064,0.127586829849962,4.43978009385641));
#21765=CARTESIAN_POINT('Ctrl Pts',(13.9710163803759,0.086208370984788,4.45178460807712));
#21766=CARTESIAN_POINT('Ctrl Pts',(13.9755103359454,0.0430996806131821,
4.45782517307841));
#21767=CARTESIAN_POINT('Ctrl Pts',(13.9800042915148,-4.68615130337092E-6,
4.45784092071359));
#21768=CARTESIAN_POINT('Origin',(12.5,0.,4.));
#21769=CARTESIAN_POINT('',(14.2800042915148,1.11332528513013E-5,4.45786561359635));
#21770=CARTESIAN_POINT('',(14.1699957084852,-1.10604184835328E-5,4.4578646218584));
#21771=CARTESIAN_POINT('',(12.5,-5.60735153159594E-17,4.457875));
#21772=CARTESIAN_POINT('Ctrl Pts',(14.1699957084852,-1.10604184835328E-5,
4.4578646218584));
#21773=CARTESIAN_POINT('Ctrl Pts',(14.1643265158203,0.0543576752587709,
4.45781404039958));
#21774=CARTESIAN_POINT('Ctrl Pts',(14.1586573231555,0.108743966382031,4.44812254260427));
#21775=CARTESIAN_POINT('Ctrl Pts',(14.1529881304907,0.159684023833442,4.42916890146099));
#21776=CARTESIAN_POINT('Ctrl Pts',(14.1451167584407,0.230411580321883,4.40285278028461));
#21777=CARTESIAN_POINT('Ctrl Pts',(14.1372453863907,0.294495541512382,4.358681244225));
#21778=CARTESIAN_POINT('Ctrl Pts',(14.1293740143408,0.344256823700223,4.30194730133701));
#21779=CARTESIAN_POINT('Ctrl Pts',(14.1215026422908,0.394018105888063,4.24521335844902));
#21780=CARTESIAN_POINT('Ctrl Pts',(14.1136312702409,0.429456709073245,4.17591700873265));
#21781=CARTESIAN_POINT('Ctrl Pts',(14.1057598981909,0.446326079279053,4.10236192849032));
#21782=CARTESIAN_POINT('Ctrl Pts',(14.097888526141,0.46319544948486,4.02880684824799));
#21783=CARTESIAN_POINT('Ctrl Pts',(14.090017154091,0.461495586711293,3.95099303747972));
#21784=CARTESIAN_POINT('Ctrl Pts',(14.0821457820411,0.441430182931853,3.87824480690492));
#21785=CARTESIAN_POINT('Ctrl Pts',(14.0742744099911,0.421364779152413,3.80549657633012));
#21786=CARTESIAN_POINT('Ctrl Pts',(14.0664030379411,0.3829338343671,3.73781392594881));
#21787=CARTESIAN_POINT('Ctrl Pts',(14.0585316658912,0.330742470300218,3.68330716492384));
#21788=CARTESIAN_POINT('Ctrl Pts',(14.0506602938412,0.278551106233337,3.62880040389886));
#21789=CARTESIAN_POINT('Ctrl Pts',(14.0427889217913,0.212599322884887,3.58746953223022));
#21790=CARTESIAN_POINT('Ctrl Pts',(14.0349175497413,0.140790022250932,3.5642671654747));
#21791=CARTESIAN_POINT('Ctrl Pts',(14.0270461776914,0.0689807216169763,
3.54106479871918));
#21792=CARTESIAN_POINT('Ctrl Pts',(14.0191748056414,-0.00868609630248519,
3.53599093687678));
#21793=CARTESIAN_POINT('Ctrl Pts',(14.0113034335915,-0.0829037347177578,
3.5496535731032));
#21794=CARTESIAN_POINT('Ctrl Pts',(14.0034320615415,-0.15712137313303,3.56331620932962));
#21795=CARTESIAN_POINT('Ctrl Pts',(13.9955606894916,-0.227889832044114,
3.59571534362485));
#21796=CARTESIAN_POINT('Ctrl Pts',(13.9876893174416,-0.286729034540398,
3.64296863695132));
#21797=CARTESIAN_POINT('Ctrl Pts',(13.9798179453916,-0.345568237036683,
3.69022193027778));
#21798=CARTESIAN_POINT('Ctrl Pts',(13.9719465733417,-0.392478183118168,
3.75232938263547));
#21799=CARTESIAN_POINT('Ctrl Pts',(13.9640752012917,-0.421837725217638,
3.82184875237013));
#21800=CARTESIAN_POINT('Ctrl Pts',(13.9562038292418,-0.451197267317109,
3.8913681221048));
#21801=CARTESIAN_POINT('Ctrl Pts',(13.9483324571918,-0.463006405434566,
3.96829940921644));
#21802=CARTESIAN_POINT('Ctrl Pts',(13.9404610851419,-0.455850068491383,
4.04342405445454));
#21803=CARTESIAN_POINT('Ctrl Pts',(13.9325897130919,-0.448693731548199,
4.11854869969265));
#21804=CARTESIAN_POINT('Ctrl Pts',(13.924718341042,-0.422571919544373,4.19186670305722));
#21805=CARTESIAN_POINT('Ctrl Pts',(13.916846968992,-0.38061476952465,4.25459247959939));
#21806=CARTESIAN_POINT('Ctrl Pts',(13.908975596942,-0.338657619504927,4.31731825614156));
#21807=CARTESIAN_POINT('Ctrl Pts',(13.9011042248921,-0.280865131469307,
4.36945180586132));
#21808=CARTESIAN_POINT('Ctrl Pts',(13.8932328528421,-0.214162491453186,
4.40474604470388));
#21809=CARTESIAN_POINT('Ctrl Pts',(13.8854871380565,-0.148524681204106,
4.43947685223224));
#21810=CARTESIAN_POINT('Ctrl Pts',(13.8777414232708,-0.0742589286223064,
4.45790169736071));
#21811=CARTESIAN_POINT('Ctrl Pts',(13.8699957084852,1.23414887176878E-6,
4.4579133809027));
#21812=CARTESIAN_POINT('Ctrl Pts',(13.9800042915148,-4.68615130337092E-6,
4.45784092071359));
#21813=CARTESIAN_POINT('Ctrl Pts',(13.9833817079953,-0.0323996211791616,
4.45785275579335));
#21814=CARTESIAN_POINT('Ctrl Pts',(13.9867591244758,-0.064792114138131,
4.45446164082457));
#21815=CARTESIAN_POINT('Ctrl Pts',(13.9901365409563,-0.0964458636128916,
4.44764173788363));
#21816=CARTESIAN_POINT('Ctrl Pts',(13.9980079130062,-0.170217765992045,
4.43174734235885));
#21817=CARTESIAN_POINT('Ctrl Pts',(14.0058792850562,-0.239977073556624,
4.39722897636055));
#21818=CARTESIAN_POINT('Ctrl Pts',(14.0137506571061,-0.297364634468633,
4.34822292324149));
#21819=CARTESIAN_POINT('Ctrl Pts',(14.0216220291561,-0.354752195380644,
4.29921687012243));
#21820=CARTESIAN_POINT('Ctrl Pts',(14.0294934012061,-0.399768009640084,
4.23572312988262));
#21821=CARTESIAN_POINT('Ctrl Pts',(14.037364773256,-0.427017900618165,4.16535006094698));
#21822=CARTESIAN_POINT('Ctrl Pts',(14.045236145306,-0.454267791596245,4.09497699201134));
#21823=CARTESIAN_POINT('Ctrl Pts',(14.0531075173559,-0.463751759292965,
4.01772459437987));
#21824=CARTESIAN_POINT('Ctrl Pts',(14.0609788894059,-0.45433335426851,3.94284990548881));
#21825=CARTESIAN_POINT('Ctrl Pts',(14.0688502614558,-0.444914949244056,
3.86797521659775));
#21826=CARTESIAN_POINT('Ctrl Pts',(14.0767216335058,-0.416594171498428,
3.7954782364471));
#21827=CARTESIAN_POINT('Ctrl Pts',(14.0845930055557,-0.372764656800254,
3.7340461680214));
#21828=CARTESIAN_POINT('Ctrl Pts',(14.0924643776057,-0.328935142102078,
3.67261409959569));
#21829=CARTESIAN_POINT('Ctrl Pts',(14.1003357496557,-0.269596890451354,
3.62224694289495));
#21830=CARTESIAN_POINT('Ctrl Pts',(14.1082071217056,-0.201860314388951,
3.58898011778223));
#21831=CARTESIAN_POINT('Ctrl Pts',(14.1160784937556,-0.134123738326549,
3.55571329266952));
#21832=CARTESIAN_POINT('Ctrl Pts',(14.1239498658055,-0.0579888378524715,
3.53954679914483));
#21833=CARTESIAN_POINT('Ctrl Pts',(14.1318212378555,0.0174212575835846,
3.54241784356498));
#21834=CARTESIAN_POINT('Ctrl Pts',(14.1396926099054,0.0928313530196406,
3.54528888798513));
#21835=CARTESIAN_POINT('Ctrl Pts',(14.1475639819554,0.167516643417675,3.56719747035013));
#21836=CARTESIAN_POINT('Ctrl Pts',(14.1554353540053,0.232527703900953,3.60551831852155));
#21837=CARTESIAN_POINT('Ctrl Pts',(14.1633067260553,0.297538764384231,3.64383916669297));
#21838=CARTESIAN_POINT('Ctrl Pts',(14.1711780981053,0.352875594952755,3.69857228067082));
#21839=CARTESIAN_POINT('Ctrl Pts',(14.1790494701552,0.391907267274456,3.76315907456484));
#21840=CARTESIAN_POINT('Ctrl Pts',(14.1869208422052,0.430938939596158,3.82774586845886));
#21841=CARTESIAN_POINT('Ctrl Pts',(14.1947922142551,0.453665453671035,3.90218634226906));
#21842=CARTESIAN_POINT('Ctrl Pts',(14.2026635863051,0.45736352584659,3.97756040711846));
#21843=CARTESIAN_POINT('Ctrl Pts',(14.210534958355,0.461061598022145,4.05293447196787));
#21844=CARTESIAN_POINT('Ctrl Pts',(14.218406330405,0.445731228298378,4.12924212785648));
#21845=CARTESIAN_POINT('Ctrl Pts',(14.2262777024549,0.413209431587385,4.19733954431574));
#21846=CARTESIAN_POINT('Ctrl Pts',(14.2341490745049,0.380687634876391,4.265436960775));
#21847=CARTESIAN_POINT('Ctrl Pts',(14.2420204465549,0.330974411178171,4.32532413780492));
#21848=CARTESIAN_POINT('Ctrl Pts',(14.2498918186048,0.270026820557645,4.36982488597043));
#21849=CARTESIAN_POINT('Ctrl Pts',(14.2577631906548,0.209079229937118,4.41432563413594));
#21850=CARTESIAN_POINT('Ctrl Pts',(14.2656345627047,0.136897272394287,4.44343995343705));
#21851=CARTESIAN_POINT('Ctrl Pts',(14.2735059347547,0.0621304022332317,
4.45367911922619));
#21852=CARTESIAN_POINT('Ctrl Pts',(14.2756720536747,0.0415553447945806,
4.4564968301158));
#21853=CARTESIAN_POINT('Ctrl Pts',(14.2778381725948,0.020784533837212,4.45788513960506));
#21854=CARTESIAN_POINT('Ctrl Pts',(14.2800042915148,1.11332528513013E-5,
4.45786561359635));
#21855=CARTESIAN_POINT('Origin',(12.5,0.,4.));
#21856=CARTESIAN_POINT('',(14.5800042915148,-1.58578451148518E-6,4.45791318879952));
#21857=CARTESIAN_POINT('',(14.4699957084852,4.96934848862042E-6,4.4578413260902));
#21858=CARTESIAN_POINT('',(12.5,-5.60735153159594E-17,4.457875));
#21859=CARTESIAN_POINT('Ctrl Pts',(14.4699957084852,4.96934848862042E-6,
4.4578413260902));
#21860=CARTESIAN_POINT('Ctrl Pts',(14.4666543524698,0.0320539454002899,
4.45785375637851));
#21861=CARTESIAN_POINT('Ctrl Pts',(14.4633129964543,0.0641003838712636,
4.45453523052653));
#21862=CARTESIAN_POINT('Ctrl Pts',(14.4599716404389,0.0954313752779353,
4.44785911407655));
#21863=CARTESIAN_POINT('Ctrl Pts',(14.452100268389,0.169239101517837,4.43213190746217));
#21864=CARTESIAN_POINT('Ctrl Pts',(14.444228896339,0.2390764403586,4.39777168651743));
#21865=CARTESIAN_POINT('Ctrl Pts',(14.4363575242891,0.296574889592956,4.34889578431359));
#21866=CARTESIAN_POINT('Ctrl Pts',(14.4284861522391,0.354073338827311,4.30001988210975));
#21867=CARTESIAN_POINT('Ctrl Pts',(14.4206147801891,0.39923289845526,4.2366282986468));
#21868=CARTESIAN_POINT('Ctrl Pts',(14.4127434081392,0.4266421670589,4.16631715105832));
#21869=CARTESIAN_POINT('Ctrl Pts',(14.4048720360892,0.454051435662541,4.09600600346984));
#21870=CARTESIAN_POINT('Ctrl Pts',(14.3970006640393,0.463710413241873,4.01877529175582));
#21871=CARTESIAN_POINT('Ctrl Pts',(14.3891292919893,0.454461679188747,3.94387945476197));
#21872=CARTESIAN_POINT('Ctrl Pts',(14.3812579199394,0.445212945135621,3.86898361776811));
#21873=CARTESIAN_POINT('Ctrl Pts',(14.3733865478894,0.417056499450037,3.79642265549441));
#21874=CARTESIAN_POINT('Ctrl Pts',(14.3655151758395,0.373366286239542,3.73489143780602));
#21875=CARTESIAN_POINT('Ctrl Pts',(14.3576438037895,0.329676073029047,3.67336022011762));
#21876=CARTESIAN_POINT('Ctrl Pts',(14.3497724317395,0.270452092293641,3.62285874701452));
#21877=CARTESIAN_POINT('Ctrl Pts',(14.3419010596896,0.202791063664024,3.58943853329022));
#21878=CARTESIAN_POINT('Ctrl Pts',(14.3340296876396,0.135130035034407,3.55601831956592));
#21879=CARTESIAN_POINT('Ctrl Pts',(14.3261583155897,0.0590319585105798,
3.53967936522043));
#21880=CARTESIAN_POINT('Ctrl Pts',(14.3182869435397,-0.0163844490157649,
3.54237954232867));
#21881=CARTESIAN_POINT('Ctrl Pts',(14.3104155714898,-0.0918008565421096,
3.54507971943691));
#21882=CARTESIAN_POINT('Ctrl Pts',(14.3025441994398,-0.166535595070972,
3.56681902799889));
#21883=CARTESIAN_POINT('Ctrl Pts',(14.2946728273899,-0.231633314431234,
3.60499247969884));
#21884=CARTESIAN_POINT('Ctrl Pts',(14.2868014553399,-0.296731033791496,
3.64316593139879));
#21885=CARTESIAN_POINT('Ctrl Pts',(14.2789300832899,-0.352191733983158,
3.6977735262367));
#21886=CARTESIAN_POINT('Ctrl Pts',(14.27105871124,-0.391369643565407,3.76227171909014));
#21887=CARTESIAN_POINT('Ctrl Pts',(14.26318733919,-0.430547553147657,3.82676991194359));
#21888=CARTESIAN_POINT('Ctrl Pts',(14.2553159671401,-0.453442672120494,
3.90115870281258));
#21889=CARTESIAN_POINT('Ctrl Pts',(14.2474445950901,-0.457311513162664,
3.97652419590847));
#21890=CARTESIAN_POINT('Ctrl Pts',(14.2395732230402,-0.461180354204834,
4.05188968900435));
#21891=CARTESIAN_POINT('Ctrl Pts',(14.2317018509902,-0.446022917316338,
4.12823188432714));
#21892=CARTESIAN_POINT('Ctrl Pts',(14.2238304789403,-0.413655495130362,
4.19640281260034));
#21893=CARTESIAN_POINT('Ctrl Pts',(14.2159591068903,-0.381288072944386,
4.26457374087354));
#21894=CARTESIAN_POINT('Ctrl Pts',(14.2080877348403,-0.33171066546093,4.32457340209717));
#21895=CARTESIAN_POINT('Ctrl Pts',(14.2002163627904,-0.270864058094251,
4.36921212802613));
#21896=CARTESIAN_POINT('Ctrl Pts',(14.1923449907404,-0.210017450727571,
4.41385085395509));
#21897=CARTESIAN_POINT('Ctrl Pts',(14.1844736186905,-0.137901643477669,
4.44312864458938));
#21898=CARTESIAN_POINT('Ctrl Pts',(14.1766022466405,-0.0631581639595259,
4.45353718675995));
#21899=CARTESIAN_POINT('Ctrl Pts',(14.1744000672554,-0.0422471272657682,
4.45644919204336));
#21900=CARTESIAN_POINT('Ctrl Pts',(14.1721978878703,-0.021130418320356,
4.45788427006097));
#21901=CARTESIAN_POINT('Ctrl Pts',(14.1699957084852,-1.10604184835328E-5,
4.4578646218584));
#21902=CARTESIAN_POINT('Ctrl Pts',(14.2800042915148,1.11332528513013E-5,
4.45786561359635));
#21903=CARTESIAN_POINT('Ctrl Pts',(14.2857095446447,-0.0547030874695854,
4.45781418483069));
#21904=CARTESIAN_POINT('Ctrl Pts',(14.2914147977746,-0.109435272994953,
4.44799629651036));
#21905=CARTESIAN_POINT('Ctrl Pts',(14.2971200509045,-0.16065599949712,4.42880599334559));
#21906=CARTESIAN_POINT('Ctrl Pts',(14.3049914229545,-0.231323748287136,
4.40232968939868));
#21907=CARTESIAN_POINT('Ctrl Pts',(14.3128627950045,-0.295307463087888,
4.35801306922771));
#21908=CARTESIAN_POINT('Ctrl Pts',(14.3207341670544,-0.344940072567234,
4.30116652609615));
#21909=CARTESIAN_POINT('Ctrl Pts',(14.3286055391044,-0.394572682046581,
4.24431998296459));
#21910=CARTESIAN_POINT('Ctrl Pts',(14.3364769111543,-0.429854186204522,
4.17494351687244));
#21911=CARTESIAN_POINT('Ctrl Pts',(14.3443482832043,-0.446556856002091,
4.10135040434572));
#21912=CARTESIAN_POINT('Ctrl Pts',(14.3522196552542,-0.46325952579966,4.027757291819));
#21913=CARTESIAN_POINT('Ctrl Pts',(14.3600910273042,-0.461383361236856,
3.9499475328577));
#21914=CARTESIAN_POINT('Ctrl Pts',(14.3679623993541,-0.441153180262727,
3.87724495265939));
#21915=CARTESIAN_POINT('Ctrl Pts',(14.3758337714041,-0.420922999288597,
3.80454237246108));
#21916=CARTESIAN_POINT('Ctrl Pts',(14.383705143454,-0.382338801903142,3.73694697102576));
#21917=CARTESIAN_POINT('Ctrl Pts',(14.391576515504,-0.330024073856894,3.68255860260764));
#21918=CARTESIAN_POINT('Ctrl Pts',(14.399447887554,-0.277709345810648,3.62817023418952));
#21919=CARTESIAN_POINT('Ctrl Pts',(14.4073192596039,-0.21166408710361,3.58698889878861));
#21920=CARTESIAN_POINT('Ctrl Pts',(14.4151906316539,-0.139802400742051,
3.56394929325792));
#21921=CARTESIAN_POINT('Ctrl Pts',(14.4230620037038,-0.0679407143804897,
3.54090968772722));
#21922=CARTESIAN_POINT('Ctrl Pts',(14.4309333757538,0.00973739963559066,
3.53601181206673));
#21923=CARTESIAN_POINT('Ctrl Pts',(14.4388047478037,0.0839238909224197,
3.54984257127538));
#21924=CARTESIAN_POINT('Ctrl Pts',(14.4466761198537,0.158110382209248,3.56367333048403));
#21925=CARTESIAN_POINT('Ctrl Pts',(14.4545474919037,0.228805250766822,3.59623272456181));
#21926=CARTESIAN_POINT('Ctrl Pts',(14.4624188639536,0.287537237904754,3.64361921078484));
#21927=CARTESIAN_POINT('Ctrl Pts',(14.4702902360036,0.346269225042686,3.69100569700788));
#21928=CARTESIAN_POINT('Ctrl Pts',(14.4781616080535,0.393038330760977,3.75321927537615));
#21929=CARTESIAN_POINT('Ctrl Pts',(14.4860329801035,0.422240284179214,3.8228049873169));
#21930=CARTESIAN_POINT('Ctrl Pts',(14.4939043521534,0.451442237597453,3.89239069925764));
#21931=CARTESIAN_POINT('Ctrl Pts',(14.5017757242034,0.463077038715637,3.96934854477086));
#21932=CARTESIAN_POINT('Ctrl Pts',(14.5096470962533,0.45575050699275,4.04445678215295));
#21933=CARTESIAN_POINT('Ctrl Pts',(14.5175184683033,0.448423975269863,4.11956501953505));
#21934=CARTESIAN_POINT('Ctrl Pts',(14.5253898403532,0.422136110705906,4.19282364878603));
#21935=CARTESIAN_POINT('Ctrl Pts',(14.5332612124032,0.380036948171907,4.2554541996672));
#21936=CARTESIAN_POINT('Ctrl Pts',(14.5411325844532,0.337937785637909,4.31808475054837));
#21937=CARTESIAN_POINT('Ctrl Pts',(14.5490039565031,0.28002732513387,4.37008722305972));
#21938=CARTESIAN_POINT('Ctrl Pts',(14.5568753285531,0.213244889156206,4.40523023992844));
#21939=CARTESIAN_POINT('Ctrl Pts',(14.5645849828737,0.147834501639678,4.43965124177167));
#21940=CARTESIAN_POINT('Ctrl Pts',(14.5722946371942,0.0739129441497101,
4.45789842831743));
#21941=CARTESIAN_POINT('Ctrl Pts',(14.5800042915148,-1.58578451148518E-6,
4.45791318879952));
#21942=CARTESIAN_POINT('Origin',(12.5,0.,4.));
#21943=CARTESIAN_POINT('',(14.8800042915148,-1.01702808208336E-5,4.45785711824254));
#21944=CARTESIAN_POINT('',(14.7699957084852,8.6346448269735E-6,4.45789857801605));
#21945=CARTESIAN_POINT('',(12.5,-5.60735153159594E-17,4.457875));
#21946=CARTESIAN_POINT('Ctrl Pts',(14.7699957084852,8.6346448269735E-6,
4.45789857801605));
#21947=CARTESIAN_POINT('Ctrl Pts',(14.7689821891192,0.00972641784825355,
4.45790700998655));
#21948=CARTESIAN_POINT('Ctrl Pts',(14.7679686697532,0.01944367562558,4.45760386164098));
#21949=CARTESIAN_POINT('Ctrl Pts',(14.7669551503872,0.0291408329004781,
4.45698549795522));
#21950=CARTESIAN_POINT('Ctrl Pts',(14.7590837783372,0.104452598317788,4.45218305332902));
#21951=CARTESIAN_POINT('Ctrl Pts',(14.7512124062873,0.178551969979598,4.4283678943965));
#21952=CARTESIAN_POINT('Ctrl Pts',(14.7433410342373,0.242559732875008,4.38839375563686));
#21953=CARTESIAN_POINT('Ctrl Pts',(14.7354696621874,0.30656749577042,4.34841961687722));
#21954=CARTESIAN_POINT('Ctrl Pts',(14.7275982901374,0.360483649899433,4.29228649829047));
#21955=CARTESIAN_POINT('Ctrl Pts',(14.7197269180875,0.397847504376097,4.22672074611392));
#21956=CARTESIAN_POINT('Ctrl Pts',(14.7118555460375,0.435211358852761,4.16115499393738));
#21957=CARTESIAN_POINT('Ctrl Pts',(14.7039841739875,0.456022913677073,4.08615660817103));
#21958=CARTESIAN_POINT('Ctrl Pts',(14.6961128019376,0.457788351878884,4.01071253147039));
#21959=CARTESIAN_POINT('Ctrl Pts',(14.6882414298876,0.459553790080695,3.93526845476975));
#21960=CARTESIAN_POINT('Ctrl Pts',(14.6803700578377,0.442273111660005,3.85937868713481));
#21961=CARTESIAN_POINT('Ctrl Pts',(14.6724986857877,0.408017034045316,3.79213698410258));
#21962=CARTESIAN_POINT('Ctrl Pts',(14.6646273137378,0.373760956430627,3.72489528107034));
#21963=CARTESIAN_POINT('Ctrl Pts',(14.6567559416878,0.32252947962194,3.6663016426408));
#21964=CARTESIAN_POINT('Ctrl Pts',(14.6488845696379,0.260461593653079,3.6233772554918));
#21965=CARTESIAN_POINT('Ctrl Pts',(14.6410131975879,0.198393707684219,3.5804528683428));
#21966=CARTESIAN_POINT('Ctrl Pts',(14.6331418255379,0.125489412555185,3.55319773247434));
#21967=CARTESIAN_POINT('Ctrl Pts',(14.625270453488,0.0504847191830214,3.54487778940425));
#21968=CARTESIAN_POINT('Ctrl Pts',(14.617399081438,-0.0245199741891427,
3.53655784633416));
#21969=CARTESIAN_POINT('Ctrl Pts',(14.6095277093881,-0.101625065804437,
3.54717309606245));
#21970=CARTESIAN_POINT('Ctrl Pts',(14.6016563373381,-0.171591169681571,
3.57545152934398));
#21971=CARTESIAN_POINT('Ctrl Pts',(14.5937849652882,-0.241557273558703,
3.6037299626255));
#21972=CARTESIAN_POINT('Ctrl Pts',(14.5859135932382,-0.304384389697674,
3.64967157946028));
#21973=CARTESIAN_POINT('Ctrl Pts',(14.5780422211883,-0.352544040227279,
3.70777126570269));
#21974=CARTESIAN_POINT('Ctrl Pts',(14.5701708491383,-0.400703690756885,
3.7658709519451));
#21975=CARTESIAN_POINT('Ctrl Pts',(14.5622994770883,-0.434195875677124,
3.83612870759516));
#21976=CARTESIAN_POINT('Ctrl Pts',(14.5544281050384,-0.449007277354457,
3.91012565253846));
#21977=CARTESIAN_POINT('Ctrl Pts',(14.5465567329884,-0.46381867903179,3.98412259748177));
#21978=CARTESIAN_POINT('Ctrl Pts',(14.5386853609385,-0.459949297466218,
4.06185873171832));
#21979=CARTESIAN_POINT('Ctrl Pts',(14.5308139888885,-0.437862794771992,
4.13401905238929));
#21980=CARTESIAN_POINT('Ctrl Pts',(14.5229426168386,-0.415776292077766,
4.20617937306026));
#21981=CARTESIAN_POINT('Ctrl Pts',(14.5150712447886,-0.375472668254887,
4.27276388016565));
#21982=CARTESIAN_POINT('Ctrl Pts',(14.5071998727387,-0.321781445311454,
4.32579385338299));
#21983=CARTESIAN_POINT('Ctrl Pts',(14.4993285006887,-0.26809022236802,4.37882382660034));
#21984=CARTESIAN_POINT('Ctrl Pts',(14.4914571286387,-0.201011400304033,
4.41829926592964));
#21985=CARTESIAN_POINT('Ctrl Pts',(14.4835857565888,-0.128582932452519,
4.43948988945229));
#21986=CARTESIAN_POINT('Ctrl Pts',(14.4790557405542,-0.0868999680795747,
4.45168520479633));
#21987=CARTESIAN_POINT('Ctrl Pts',(14.4745257245197,-0.0434451672832877,
4.45782447382869));
#21988=CARTESIAN_POINT('Ctrl Pts',(14.4699957084852,4.96934848862042E-6,
4.4578413260902));
#21989=CARTESIAN_POINT('Ctrl Pts',(14.5800042915148,-1.58578451148518E-6,
4.45791318879952));
#21990=CARTESIAN_POINT('Ctrl Pts',(14.5801660092442,-0.00155201715944126,
4.45791349841543));
#21991=CARTESIAN_POINT('Ctrl Pts',(14.5803277269736,-0.00310244544229786,
4.45790578589721));
#21992=CARTESIAN_POINT('Ctrl Pts',(14.5804894447029,-0.0046527920161852,
4.45789003224535));
#21993=CARTESIAN_POINT('Ctrl Pts',(14.5883608167529,-0.0801136257596197,
4.45712324646747));
#21994=CARTESIAN_POINT('Ctrl Pts',(14.5962321888029,-0.155380881795201,
4.43730611368561));
#21995=CARTESIAN_POINT('Ctrl Pts',(14.6041035608528,-0.22143539919095,4.4008132908088));
#21996=CARTESIAN_POINT('Ctrl Pts',(14.6119749329028,-0.287489916586699,
4.36432046793199));
#21997=CARTESIAN_POINT('Ctrl Pts',(14.6198463049527,-0.344331695342615,
4.31115195496024));
#21998=CARTESIAN_POINT('Ctrl Pts',(14.6277176770027,-0.38514947146564,4.24767885402976));
#21999=CARTESIAN_POINT('Ctrl Pts',(14.6355890490526,-0.425967247588666,
4.18420575309928));
#22000=CARTESIAN_POINT('Ctrl Pts',(14.6434604211026,-0.4507610210788,4.11042806421008));
#22001=CARTESIAN_POINT('Ctrl Pts',(14.6513317931525,-0.45655979174196,4.03518645571321));
#22002=CARTESIAN_POINT('Ctrl Pts',(14.6592031652025,-0.462358562405121,
3.95994484721634));
#22003=CARTESIAN_POINT('Ctrl Pts',(14.6670745372524,-0.449162330241309,
3.8832393191118));
#22004=CARTESIAN_POINT('Ctrl Pts',(14.6749459093024,-0.41855237967279,3.81426137832517));
#22005=CARTESIAN_POINT('Ctrl Pts',(14.6828172813524,-0.387942429104271,
3.74528343753854));
#22006=CARTESIAN_POINT('Ctrl Pts',(14.6906886534023,-0.339918760131043,
3.68403308406983));
#22007=CARTESIAN_POINT('Ctrl Pts',(14.6985600254523,-0.280235976103336,
3.63784985464301));
#22008=CARTESIAN_POINT('Ctrl Pts',(14.7064313975022,-0.220553192075631,
3.5916666252162));
#22009=CARTESIAN_POINT('Ctrl Pts',(14.7143027695522,-0.149211292993445,
3.5605505198313));
#22010=CARTESIAN_POINT('Ctrl Pts',(14.7221741416021,-0.0747590701011626,
3.54823013427646));
#22011=CARTESIAN_POINT('Ctrl Pts',(14.7300455136521,-0.000306847208877067,
3.53590974872161));
#22012=CARTESIAN_POINT('Ctrl Pts',(14.737916885702,0.0772556994935079,3.54238508299684));
#22013=CARTESIAN_POINT('Ctrl Pts',(14.745788257752,0.148634367597872,3.5668802073009));
#22014=CARTESIAN_POINT('Ctrl Pts',(14.753659629802,0.220013035702235,3.59137533160497));
#22015=CARTESIAN_POINT('Ctrl Pts',(14.7615310018519,0.285207825208577,3.63389024593787));
#22016=CARTESIAN_POINT('Ctrl Pts',(14.7694023739019,0.336406544142474,3.68933045342307));
#22017=CARTESIAN_POINT('Ctrl Pts',(14.7772737459518,0.387605263076371,3.74477066090827));
#22018=CARTESIAN_POINT('Ctrl Pts',(14.7851451180018,0.424807911437823,3.81313616154577));
#22019=CARTESIAN_POINT('Ctrl Pts',(14.7930164900517,0.443556551112275,3.88623481973509));
#22020=CARTESIAN_POINT('Ctrl Pts',(14.8008878621017,0.462305190786727,3.9593334779244));
#22021=CARTESIAN_POINT('Ctrl Pts',(14.8087592341516,0.462599821774179,4.03716529366552));
#22022=CARTESIAN_POINT('Ctrl Pts',(14.8166306062016,0.444405141642572,4.11040380200553));
#22023=CARTESIAN_POINT('Ctrl Pts',(14.8245019782516,0.426210461510966,4.18364231034555));
#22024=CARTESIAN_POINT('Ctrl Pts',(14.8323733503015,0.389526470260302,4.25228751128446));
#22025=CARTESIAN_POINT('Ctrl Pts',(14.8402447223515,0.338748948932789,4.3081137476731));
#22026=CARTESIAN_POINT('Ctrl Pts',(14.8481160944014,0.287971427605278,4.36393998406173));
#22027=CARTESIAN_POINT('Ctrl Pts',(14.8559874664514,0.22310037620092,4.40694725590009));
#22028=CARTESIAN_POINT('Ctrl Pts',(14.8638588385013,0.151909206873508,4.43198208217373));
#22029=CARTESIAN_POINT('Ctrl Pts',(14.8692406561725,0.103234351881841,4.44909890368578));
#22030=CARTESIAN_POINT('Ctrl Pts',(14.8746224738437,0.0516050086776526,
4.45781408155485));
#22031=CARTESIAN_POINT('Ctrl Pts',(14.8800042915148,-1.01702808208336E-5,
4.45785711824254));
#22032=CARTESIAN_POINT('Origin',(12.5,0.,4.));
#22033=CARTESIAN_POINT('',(15.1,-5.60735153159594E-17,4.457875));
#22034=CARTESIAN_POINT('',(15.0699957084852,-1.05870731373636E-5,4.45788944868556));
#22035=CARTESIAN_POINT('',(12.5,-5.60735153159594E-17,4.457875));
#22036=CARTESIAN_POINT('',(15.1,-0.269165465906718,4.37040446485999));
#22037=CARTESIAN_POINT('Origin',(15.1,0.,4.));
#22038=CARTESIAN_POINT('Ctrl Pts',(15.1,-0.269173508333955,4.37043259773194));
#22039=CARTESIAN_POINT('Ctrl Pts',(15.0991842588284,-0.262849866117432,
4.37503549456412));
#22040=CARTESIAN_POINT('Ctrl Pts',(15.0983685176569,-0.256407545646713,
4.37947450812006));
#22041=CARTESIAN_POINT('Ctrl Pts',(15.0975527764853,-0.249853611926923,
4.38374199825787));
#22042=CARTESIAN_POINT('Ctrl Pts',(15.0896814044354,-0.186612411779406,
4.42492050409441));
#22043=CARTESIAN_POINT('Ctrl Pts',(15.0818100323854,-0.112978907049287,
4.45012847221118));
#22044=CARTESIAN_POINT('Ctrl Pts',(15.0739386603355,-0.0377721395608013,
4.45635245505497));
#22045=CARTESIAN_POINT('Ctrl Pts',(15.072624343052,-0.0252145379490987,
4.45739170058566));
#22046=CARTESIAN_POINT('Ctrl Pts',(15.0713100257686,-0.0126130730861363,
4.45790166433459));
#22047=CARTESIAN_POINT('Ctrl Pts',(15.0699957084852,-1.05870731373636E-5,
4.45788944868556));
#22048=CARTESIAN_POINT('Origin',(11.8752146997001,0.,4.));
#22049=CARTESIAN_POINT('',(14.9247853002999,-1.38824472118437E-5,4.62497559137666));
#22050=CARTESIAN_POINT('',(15.0252146997001,-1.44513692928093E-5,4.62501972247551));
#22051=CARTESIAN_POINT('',(11.8752146997001,-1.68747709936658E-14,4.625));
#22052=CARTESIAN_POINT('',(15.1,-0.624993681275899,4.00281040303151));
#22053=CARTESIAN_POINT('Ctrl Pts',(15.0252146997001,-1.44513692928189E-5,
4.62501972247551));
#22054=CARTESIAN_POINT('Ctrl Pts',(15.0265290169835,-0.017216861979444,
4.62503639685311));
#22055=CARTESIAN_POINT('Ctrl Pts',(15.0357147063169,-0.137433797398843,
4.62017138475037));
#22056=CARTESIAN_POINT('Ctrl Pts',(15.0527717677003,-0.355236031271534,
4.54560815721762));
#22057=CARTESIAN_POINT('Ctrl Pts',(15.0763858838501,-0.571652475026301,
4.31158258982903));
#22058=CARTESIAN_POINT('Ctrl Pts',(15.09212862795,-0.624530364890795,4.10584538053252));
#22059=CARTESIAN_POINT('Ctrl Pts',(15.1,-0.624993681275899,4.00281040303152));
#22060=CARTESIAN_POINT('',(15.1,0.314930721058197,3.46014479632612));
#22061=CARTESIAN_POINT('Origin',(15.1,0.,4.));
#22062=CARTESIAN_POINT('Ctrl Pts',(14.9247853002999,-1.38824472118368E-5,
4.62497559137666));
#22063=CARTESIAN_POINT('Ctrl Pts',(14.9272748546787,-0.0326052931943186,
4.62500276606431));
#22064=CARTESIAN_POINT('Ctrl Pts',(14.9376357811074,-0.168225686180582,
4.61457389311938));
#22065=CARTESIAN_POINT('Ctrl Pts',(14.9558680795861,-0.394527586443172,
4.517903766532));
#22066=CARTESIAN_POINT('Ctrl Pts',(14.979482195736,-0.593077772790822,4.26857965265179));
#22067=CARTESIAN_POINT('Ctrl Pts',(15.0030963118859,-0.649493436571599,
3.95488773069898));
#22068=CARTESIAN_POINT('Ctrl Pts',(15.0267104280357,-0.550252000240565,
3.65200904506483));
#22069=CARTESIAN_POINT('Ctrl Pts',(15.0503245441856,-0.319142060764588,
3.43252503194012));
#22070=CARTESIAN_POINT('Ctrl Pts',(15.0739386603355,-0.0115409051696555,
3.34904846156061));
#22071=CARTESIAN_POINT('Ctrl Pts',(15.0904971456069,0.20608092381284,3.39989411918499));
#22072=CARTESIAN_POINT('Ctrl Pts',(15.0991842588284,0.305720220830039,3.45471854406458));
#22073=CARTESIAN_POINT('Ctrl Pts',(15.1,0.314937815442301,3.46010549098218));
#22074=CARTESIAN_POINT('Origin',(11.8752146997001,0.,4.));
#22075=CARTESIAN_POINT('',(14.6247853002999,-2.16459804047719E-6,4.62505212776347));
#22076=CARTESIAN_POINT('',(14.7252146997001,1.17863019661874E-5,4.62503218402409));
#22077=CARTESIAN_POINT('',(11.8752146997001,-1.68747709936658E-14,4.625));
#22078=CARTESIAN_POINT('Ctrl Pts',(14.7252146997001,1.17863019662174E-5,
4.62503218402409));
#22079=CARTESIAN_POINT('Ctrl Pts',(14.7320725523841,-0.0897427467603322,
4.62495430540108));
#22080=CARTESIAN_POINT('Ctrl Pts',(14.746801777118,-0.282587126126967,4.58296482291278));
#22081=CARTESIAN_POINT('Ctrl Pts',(14.7694023739019,-0.520130285395982,
4.39158760667368));
#22082=CARTESIAN_POINT('Ctrl Pts',(14.7930164900517,-0.64367318065081,4.09778141619902));
#22083=CARTESIAN_POINT('Ctrl Pts',(14.8166306062016,-0.612955311082805,
3.78054123783642));
#22084=CARTESIAN_POINT('Ctrl Pts',(14.8402447223515,-0.435338447621071,
3.51589585985611));
#22085=CARTESIAN_POINT('Ctrl Pts',(14.8638588385013,-0.153389665944836,
3.36726945127358));
#22086=CARTESIAN_POINT('Ctrl Pts',(14.8874729546512,0.165319955489652,3.37028123293502));
#22087=CARTESIAN_POINT('Ctrl Pts',(14.9110870708011,0.444409630539555,3.52420969451069));
#22088=CARTESIAN_POINT('Ctrl Pts',(14.9347011869509,0.616993161964042,3.79216419995926));
#22089=CARTESIAN_POINT('Ctrl Pts',(14.9583153031008,0.641710593195818,4.10992889087348));
#22090=CARTESIAN_POINT('Ctrl Pts',(14.9819294192507,0.512636325700993,4.40134645341462));
#22091=CARTESIAN_POINT('Ctrl Pts',(15.0042292181171,0.274729866520086,4.58571614948967));
#22092=CARTESIAN_POINT('Ctrl Pts',(15.0186576449336,0.0858074045169303,
4.62493653494651));
#22093=CARTESIAN_POINT('Ctrl Pts',(15.0252146997001,-1.44513692928189E-5,
4.62501972247551));
#22094=CARTESIAN_POINT('Ctrl Pts',(14.6247853002999,-2.16459804049194E-6,
4.62505212776347));
#22095=CARTESIAN_POINT('Ctrl Pts',(14.6249470180292,-0.00211850554115318,
4.62505255038961));
#22096=CARTESIAN_POINT('Ctrl Pts',(14.6329801078086,-0.107244412024774,
4.62452960748548));
#22097=CARTESIAN_POINT('Ctrl Pts',(14.6488845696379,-0.314835022974042,
4.56987302880665));
#22098=CARTESIAN_POINT('Ctrl Pts',(14.6724986857877,-0.547602339746838,
4.35214775046202));
#22099=CARTESIAN_POINT('Ctrl Pts',(14.6961128019376,-0.649132943719538,
4.05002781234082));
#22100=CARTESIAN_POINT('Ctrl Pts',(14.7197269180875,-0.595094318970103,
3.73591836064326));
#22101=CARTESIAN_POINT('Ctrl Pts',(14.7433410342373,-0.398437197867616,
3.48509791236843));
#22102=CARTESIAN_POINT('Ctrl Pts',(14.7669551503872,-0.1062918289807,3.35767733339665));
#22103=CARTESIAN_POINT('Ctrl Pts',(14.7905692665371,0.211327117384507,3.38419385377023));
#22104=CARTESIAN_POINT('Ctrl Pts',(14.8141833826869,0.478300047385911,3.5582926020622));
#22105=CARTESIAN_POINT('Ctrl Pts',(14.8377974988368,0.630645044771057,3.83824960712979));
#22106=CARTESIAN_POINT('Ctrl Pts',(14.8614116149867,0.631851559871185,4.15697121131127));
#22107=CARTESIAN_POINT('Ctrl Pts',(14.8850257311365,0.481630465478622,4.4380735902585));
#22108=CARTESIAN_POINT('Ctrl Pts',(14.9061502929076,0.243989509668873,4.59562135563586));
#22109=CARTESIAN_POINT('Ctrl Pts',(14.9194034826287,0.0704409072858971,
4.62491684623921));
#22110=CARTESIAN_POINT('Ctrl Pts',(14.9247853002999,-1.38824472118368E-5,
4.62497559137666));
#22111=CARTESIAN_POINT('Origin',(11.8752146997001,0.,4.));
#22112=CARTESIAN_POINT('',(14.3247853002999,1.51969053300144E-5,4.6249871875462));
#22113=CARTESIAN_POINT('',(14.4252146997001,6.78316748347314E-6,4.62495403506715));
#22114=CARTESIAN_POINT('',(11.8752146997001,-1.68747709936658E-14,4.625));
#22115=CARTESIAN_POINT('Ctrl Pts',(14.4252146997001,6.78316748347826E-6,
4.62495403506715));
#22116=CARTESIAN_POINT('Ctrl Pts',(14.4297447157347,-0.0593027126443913,
4.62493103170719));
#22117=CARTESIAN_POINT('Ctrl Pts',(14.4421461038192,-0.221686029527806,
4.60198961095629));
#22118=CARTESIAN_POINT('Ctrl Pts',(14.4624188639536,-0.457506203155893,
4.46321101183598));
#22119=CARTESIAN_POINT('Ctrl Pts',(14.4860329801035,-0.622549707754089,
4.19054718257559));
#22120=CARTESIAN_POINT('Ctrl Pts',(14.5096470962533,-0.63839484111024,3.87221739454711));
#22121=CARTESIAN_POINT('Ctrl Pts',(14.5332612124032,-0.501244206711231,
3.58451159745434));
#22122=CARTESIAN_POINT('Ctrl Pts',(14.5568753285531,-0.243966908844842,
3.39638048838484));
#22123=CARTESIAN_POINT('Ctrl Pts',(14.5804894447029,0.0717787570654544,
3.35291099727801));
#22124=CARTESIAN_POINT('Ctrl Pts',(14.6041035608528,0.370322144162233,3.46452089026927));
#22125=CARTESIAN_POINT('Ctrl Pts',(14.6277176770027,0.580115251486915,3.70446207957941));
#22126=CARTESIAN_POINT('Ctrl Pts',(14.6513317931525,0.650879700384091,4.0152309888134));
#22127=CARTESIAN_POINT('Ctrl Pts',(14.6749459093024,0.565656298155129,4.32234968564526));
#22128=CARTESIAN_POINT('Ctrl Pts',(14.6985600254523,0.344869426209941,4.55221503612336));
#22129=CARTESIAN_POINT('Ctrl Pts',(14.7153162889182,0.129554394067723,4.62141618582314));
#22130=CARTESIAN_POINT('Ctrl Pts',(14.7242011803341,0.0132765736394338,
4.62504369367533));
#22131=CARTESIAN_POINT('Ctrl Pts',(14.7252146997001,1.17863019662174E-5,
4.62503218402409));
#22132=CARTESIAN_POINT('Ctrl Pts',(14.3247853002999,1.51969053300109E-5,
4.6249871875462));
#22133=CARTESIAN_POINT('Ctrl Pts',(14.3304905534298,-0.0746697890657793,
4.62491698721088));
#22134=CARTESIAN_POINT('Ctrl Pts',(14.3440671786096,-0.252453835406249,
4.59302599116618));
#22135=CARTESIAN_POINT('Ctrl Pts',(14.3655151758395,-0.490432948250941,
4.42819608115853));
#22136=CARTESIAN_POINT('Ctrl Pts',(14.3891292919893,-0.634910852255616,
4.14409916841427));
#22137=CARTESIAN_POINT('Ctrl Pts',(14.4127434081392,-0.627227950688033,
3.82546788683648));
#22138=CARTESIAN_POINT('Ctrl Pts',(14.4363575242891,-0.469225504392149,
3.54866444115539));
#22139=CARTESIAN_POINT('Ctrl Pts',(14.4599716404389,-0.198769899531221,
3.38002670405092));
#22140=CARTESIAN_POINT('Ctrl Pts',(14.4835857565888,0.11932229545683,3.35996988316441));
#22141=CARTESIAN_POINT('Ctrl Pts',(14.5071998727387,0.408818071695872,3.49330073524378));
#22142=CARTESIAN_POINT('Ctrl Pts',(14.5308139888885,0.600337751131954,3.74806559342675));
#22143=CARTESIAN_POINT('Ctrl Pts',(14.5544281050384,0.647982309355475,4.06320828594604));
#22144=CARTESIAN_POINT('Ctrl Pts',(14.5780422211883,0.540333396317157,4.36320267272319));
#22145=CARTESIAN_POINT('Ctrl Pts',(14.6014946196088,0.304813865567294,4.57469465218781));
#22146=CARTESIAN_POINT('Ctrl Pts',(14.6170756459793,0.100891269655612,4.62503197968527));
#22147=CARTESIAN_POINT('Ctrl Pts',(14.6247853002999,-2.16459804049194E-6,
4.62505212776347));
#22148=CARTESIAN_POINT('Origin',(11.8752146997001,0.,4.));
#22149=CARTESIAN_POINT('',(14.0247853002999,-6.3966029390794E-6,4.62495348172753));
#22150=CARTESIAN_POINT('',(14.1252146997001,-1.50974863142078E-5,4.62498583382255));
#22151=CARTESIAN_POINT('',(11.8752146997001,-1.68747709936658E-14,4.625));
#22152=CARTESIAN_POINT('Ctrl Pts',(14.1252146997001,-1.50974863141889E-5,
4.62498583382255));
#22153=CARTESIAN_POINT('Ctrl Pts',(14.1274168790852,-0.0288430498503269,
4.62501265364587));
#22154=CARTESIAN_POINT('Ctrl Pts',(14.1374904305203,-0.160695812902997,
4.61605202430223));
#22155=CARTESIAN_POINT('Ctrl Pts',(14.1554353540053,-0.385112282251534,
4.52494275637564));
#22156=CARTESIAN_POINT('Ctrl Pts',(14.1790494701552,-0.588131968915973,
4.27924389796604));
#22157=CARTESIAN_POINT('Ctrl Pts',(14.2026635863051,-0.65020173504413,3.96662229549764));
#22158=CARTESIAN_POINT('Ctrl Pts',(14.2262777024549,-0.556446129094758,
3.66199989226673));
#22159=CARTESIAN_POINT('Ctrl Pts',(14.2498918186048,-0.329334334698108,
3.43838156778717));
#22160=CARTESIAN_POINT('Ctrl Pts',(14.2735059347547,-0.0232952743833569,
3.34935901020328));
#22161=CARTESIAN_POINT('Ctrl Pts',(14.2971200509045,0.28832666060365,3.41626709515619));
#22162=CARTESIAN_POINT('Ctrl Pts',(14.3207341670544,0.530849104237583,3.62307083431711));
#22163=CARTESIAN_POINT('Ctrl Pts',(14.3443482832043,0.646149864620809,3.92020827196535));
#22164=CARTESIAN_POINT('Ctrl Pts',(14.3679623993541,0.606596311879891,4.2364683526943));
#22165=CARTESIAN_POINT('Ctrl Pts',(14.391576515504,0.42166773027486,4.49605714656388));
#22166=CARTESIAN_POINT('Ctrl Pts',(14.4106606156193,0.190545343529355,4.60977018898031));
#22167=CARTESIAN_POINT('Ctrl Pts',(14.4218733436847,0.0437536792250838,
4.62497100242767));
#22168=CARTESIAN_POINT('Ctrl Pts',(14.4252146997001,6.78316748347826E-6,
4.62495403506715));
#22169=CARTESIAN_POINT('Ctrl Pts',(14.0247853002999,-6.39660293913491E-6,
4.62495348172753));
#22170=CARTESIAN_POINT('Ctrl Pts',(14.0281627167804,-0.0442255271350925,
4.62496963662755));
#22171=CARTESIAN_POINT('Ctrl Pts',(14.0394115053108,-0.191490205391595,
4.6095527480466));
#22172=CARTESIAN_POINT('Ctrl Pts',(14.0585316658912,-0.422790583021024,
4.49510047824495));
#22173=CARTESIAN_POINT('Ctrl Pts',(14.0821457820411,-0.60713052675338,4.23509335195577));
#22174=CARTESIAN_POINT('Ctrl Pts',(14.1057598981909,-0.645967413308333,
3.91874446730605));
#22175=CARTESIAN_POINT('Ctrl Pts',(14.1293740143408,-0.529993712466286,
3.62186903671368));
#22176=CARTESIAN_POINT('Ctrl Pts',(14.1529881304907,-0.287003328966194,
3.41561532377041));
#22177=CARTESIAN_POINT('Ctrl Pts',(14.1766022466405,0.0247694002478971,
3.34941346658496));
#22178=CARTESIAN_POINT('Ctrl Pts',(14.2002163627904,0.330605970264406,3.43912920108534));
#22179=CARTESIAN_POINT('Ctrl Pts',(14.2238304789403,0.557210518047066,3.66326152695696));
#22180=CARTESIAN_POINT('Ctrl Pts',(14.2474445950901,0.650275686248857,3.96809557204375));
#22181=CARTESIAN_POINT('Ctrl Pts',(14.27105871124,0.587497759452106,4.28057573538778));
#22182=CARTESIAN_POINT('Ctrl Pts',(14.2946728273899,0.383921904832036,4.52581397056352));
#22183=CARTESIAN_POINT('Ctrl Pts',(14.3125816904098,0.159750963363977,4.61623247111552));
#22184=CARTESIAN_POINT('Ctrl Pts',(14.3226191813798,0.0283709170587055,
4.62501384057475));
#22185=CARTESIAN_POINT('Ctrl Pts',(14.3247853002999,1.51969053300109E-5,
4.6249871875462));
#22186=CARTESIAN_POINT('Origin',(11.8752146997001,0.,4.));
#22187=CARTESIAN_POINT('',(13.7247853002999,-1.20831421157597E-5,4.62503091248755));
#22188=CARTESIAN_POINT('',(13.8252146997001,1.68461488569462E-6,4.62505238998457));
#22189=CARTESIAN_POINT('',(11.8752146997001,-1.68747709936658E-14,4.625));
#22190=CARTESIAN_POINT('Ctrl Pts',(13.8252146997001,1.68461488569581E-6,
4.62505238998457));
#22191=CARTESIAN_POINT('Ctrl Pts',(13.8329604144858,-0.101363538932993,
4.62503644193381));
#22192=CARTESIAN_POINT('Ctrl Pts',(13.8485775013214,-0.305753798836605,
4.57432856173903));
#22193=CARTESIAN_POINT('Ctrl Pts',(13.8720659602069,-0.541154937947787,
4.36197748624323));
#22194=CARTESIAN_POINT('Ctrl Pts',(13.8956800763568,-0.648123865072376,
4.06173996222779));
#22195=CARTESIAN_POINT('Ctrl Pts',(13.9192941925067,-0.599765396122921,
3.74670602647169));
#22196=CARTESIAN_POINT('Ctrl Pts',(13.9429083086565,-0.407668974822819,
3.49237575473668));
#22197=CARTESIAN_POINT('Ctrl Pts',(13.9665224248064,-0.117871845784803,
3.35970116712309));
#22198=CARTESIAN_POINT('Ctrl Pts',(13.9901365409563,0.200174091641329,3.38047865214521));
#22199=CARTESIAN_POINT('Ctrl Pts',(14.0137506571061,0.470246914526057,3.54972874087838));
#22200=CARTESIAN_POINT('Ctrl Pts',(14.037364773256,0.627621790796785,3.82688947135059));
#22201=CARTESIAN_POINT('Ctrl Pts',(14.0609788894059,0.634582735815489,4.14553734509456));
#22202=CARTESIAN_POINT('Ctrl Pts',(14.0845930055557,0.489461510650943,4.42930618095194));
#22203=CARTESIAN_POINT('Ctrl Pts',(14.1060049423205,0.251510284961593,4.59332024860173));
#22204=CARTESIAN_POINT('Ctrl Pts',(14.1195455070353,0.074198300926532,4.62491679006221));
#22205=CARTESIAN_POINT('Ctrl Pts',(14.1252146997001,-1.50974863141889E-5,
4.62498583382255));
#22206=CARTESIAN_POINT('Ctrl Pts',(13.7247853002999,-1.20831421156938E-5,
4.62503091248755));
#22207=CARTESIAN_POINT('Ctrl Pts',(13.7258348801309,-0.013748904810447,
4.62504304225186));
#22208=CARTESIAN_POINT('Ctrl Pts',(13.734755832012,-0.130498998332177,4.62127102305724));
#22209=CARTESIAN_POINT('Ctrl Pts',(13.7515481559429,-0.346119716157775,
4.55143222859795));
#22210=CARTESIAN_POINT('Ctrl Pts',(13.7751622720928,-0.566385203513325,
4.32106722332061));
#22211=CARTESIAN_POINT('Ctrl Pts',(13.7987763882427,-0.650912534047929,
4.01375622291695));
#22212=CARTESIAN_POINT('Ctrl Pts',(13.8223905043925,-0.57944414457563,3.70314844792952));
#22213=CARTESIAN_POINT('Ctrl Pts',(13.8460046205424,-0.369107932149097,
3.46368321387984));
#22214=CARTESIAN_POINT('Ctrl Pts',(13.8696187366923,-0.0703124342978696,
3.35275003110641));
#22215=CARTESIAN_POINT('Ctrl Pts',(13.8932328528421,0.245333927901481,3.3969348091043));
#22216=CARTESIAN_POINT('Ctrl Pts',(13.916846968992,0.502184306426786,3.58564835824111));
#22217=CARTESIAN_POINT('Ctrl Pts',(13.9404610851419,0.638682720042094,3.87366416276737));
#22218=CARTESIAN_POINT('Ctrl Pts',(13.9640752012917,0.62211637371287,4.19195723015293));
#22219=CARTESIAN_POINT('Ctrl Pts',(13.9876893174416,0.456455507660852,4.46424641105313));
#22220=CARTESIAN_POINT('Ctrl Pts',(14.007926017111,0.220741531225703,4.60224444133776));
#22221=CARTESIAN_POINT('Ctrl Pts',(14.0202913447304,0.058831122868106,4.62493198618401));
#22222=CARTESIAN_POINT('Ctrl Pts',(14.0247853002999,-6.39660293913491E-6,
4.62495348172753));
#22223=CARTESIAN_POINT('Origin',(11.8752146997001,0.,4.));
#22224=CARTESIAN_POINT('',(13.4247853002999,1.36962628664028E-5,4.62502243215823));
#22225=CARTESIAN_POINT('',(13.5252146997001,1.40828270379035E-5,4.62497680637469));
#22226=CARTESIAN_POINT('',(11.8752146997001,-1.68747709936658E-14,4.625));
#22227=CARTESIAN_POINT('Ctrl Pts',(13.5252146997001,1.4082827037902E-5,
4.62497680637469));
#22228=CARTESIAN_POINT('Ctrl Pts',(13.5306325778363,-0.0709123884867814,
4.62491668074428));
#22229=CARTESIAN_POINT('Ctrl Pts',(13.5439218280225,-0.244933372371362,
4.59533688876844));
#22230=CARTESIAN_POINT('Ctrl Pts',(13.5650824502587,-0.482621788093898,
4.43698120905743));
#22231=CARTESIAN_POINT('Ctrl Pts',(13.5886965664085,-0.632205603168059,
4.15553919999523));
#22232=CARTESIAN_POINT('Ctrl Pts',(13.6123106825584,-0.630276944445953,
3.83682113889318));
#22233=CARTESIAN_POINT('Ctrl Pts',(13.6359247987083,-0.477298028416376,
3.55721002779864));
#22234=CARTESIAN_POINT('Ctrl Pts',(13.6595389148582,-0.209931317243796,
3.38371661595291));
#22235=CARTESIAN_POINT('Ctrl Pts',(13.683153031008,0.107746895509167,3.35791980725116));
#22236=CARTESIAN_POINT('Ctrl Pts',(13.7067671471579,0.399602814690774,3.48600198647908));
#22237=CARTESIAN_POINT('Ctrl Pts',(13.7303812633077,0.59569113756138,3.73726736776131));
#22238=CARTESIAN_POINT('Ctrl Pts',(13.7539953794576,0.649017932507905,4.05149845333026));
#22239=CARTESIAN_POINT('Ctrl Pts',(13.7776094956075,0.546803061895555,4.35338757606046));
#22240=CARTESIAN_POINT('Ctrl Pts',(13.8012236117573,0.313543031018869,4.57058490613733));
#22241=CARTESIAN_POINT('Ctrl Pts',(13.8170920131216,0.106300066848774,4.6246481407235));
#22242=CARTESIAN_POINT('Ctrl Pts',(13.8250890424358,0.00164611344283092,
4.62505264870678));
#22243=CARTESIAN_POINT('Ctrl Pts',(13.8252146997001,1.68461488569581E-6,
4.62505238998457));
#22244=CARTESIAN_POINT('Ctrl Pts',(13.4247853002999,1.36962628664097E-5,
4.62502243215823));
#22245=CARTESIAN_POINT('Ctrl Pts',(13.4313784155315,-0.086279884022628,
4.62493973056585));
#22246=CARTESIAN_POINT('Ctrl Pts',(13.445842902813,-0.275670893367246,4.58538934244717));
#22247=CARTESIAN_POINT('Ctrl Pts',(13.4681787621445,-0.513544980480383,
4.40018484937968));
#22248=CARTESIAN_POINT('Ctrl Pts',(13.4917928782944,-0.64195771209056,4.10847422061066));
#22249=CARTESIAN_POINT('Ctrl Pts',(13.5154069944443,-0.616520809113462,
3.79076698974655));
#22250=CARTESIAN_POINT('Ctrl Pts',(13.5390211105941,-0.443330402422436,
3.52320390633144));
#22251=CARTESIAN_POINT('Ctrl Pts',(13.562635226744,-0.163892778617988,3.36990832590288));
#22252=CARTESIAN_POINT('Ctrl Pts',(13.5862493428939,0.154822890495328,3.36761860145296));
#22253=CARTESIAN_POINT('Ctrl Pts',(13.6098634590437,0.43643417612693,3.51688348138565));
#22254=CARTESIAN_POINT('Ctrl Pts',(13.6334775751936,0.613450973283793,3.78193059814177));
#22255=CARTESIAN_POINT('Ctrl Pts',(13.6570916913435,0.643449974253473,4.09923956510808));
#22256=CARTESIAN_POINT('Ctrl Pts',(13.6807058074933,0.519241709620395,4.39276507945606));
#22257=CARTESIAN_POINT('Ctrl Pts',(13.7032703438121,0.281645253009076,4.58329909926801));
#22258=CARTESIAN_POINT('Ctrl Pts',(13.717963508081,0.0892710189108511,4.62495207452848));
#22259=CARTESIAN_POINT('Ctrl Pts',(13.7247853002999,-1.20831421156938E-5,
4.62503091248755));
#22260=CARTESIAN_POINT('Origin',(11.8752146997001,0.,4.));
#22261=CARTESIAN_POINT('',(13.1247853002999,3.84888821539087E-6,4.62495078081483));
#22262=CARTESIAN_POINT('',(13.2252146997001,-9.32440196476731E-6,4.62495874418382));
#22263=CARTESIAN_POINT('',(11.8752146997001,-1.68747709936658E-14,4.625));
#22264=CARTESIAN_POINT('Ctrl Pts',(13.2252146997001,-9.32440196474427E-6,
4.62495874418382));
#22265=CARTESIAN_POINT('Ctrl Pts',(13.2283047411869,-0.040464997295585,
4.62498052751194));
#22266=CARTESIAN_POINT('Ctrl Pts',(13.2392661547237,-0.18396024524725,4.61125364372682));
#22267=CARTESIAN_POINT('Ctrl Pts',(13.2580989403104,-0.413782468289504,
4.50265339583901));
#22268=CARTESIAN_POINT('Ctrl Pts',(13.2817130564603,-0.602786876612853,
4.24601696851145));
#22269=CARTESIAN_POINT('Ctrl Pts',(13.3053271726101,-0.647329213752593,
3.9304208620728));
#22270=CARTESIAN_POINT('Ctrl Pts',(13.32894128876,-0.536734598538914,3.6314998804023));
#22271=CARTESIAN_POINT('Ctrl Pts',(13.3525554049099,-0.297507800394296,
3.42089251764738));
#22272=CARTESIAN_POINT('Ctrl Pts',(13.3761695210598,0.0130188131672444,
3.34907229440132));
#22273=CARTESIAN_POINT('Ctrl Pts',(13.3997836372096,0.320425377524893,3.43325142712992));
#22274=CARTESIAN_POINT('Ctrl Pts',(13.4233977533595,0.551039769569266,3.65325580067535));
#22275=CARTESIAN_POINT('Ctrl Pts',(13.4470118695093,0.649593644862141,3.95635983539258));
#22276=CARTESIAN_POINT('Ctrl Pts',(13.4706259856592,0.592467881122722,4.26992253935193));
#22277=CARTESIAN_POINT('Ctrl Pts',(13.4942401018091,0.393353065302923,4.5187964277335));
#22278=CARTESIAN_POINT('Ctrl Pts',(13.5124363398227,0.1672808180195,4.61476328251587));
#22279=CARTESIAN_POINT('Ctrl Pts',(13.5227612057864,0.0321332374692893,
4.62500403435298));
#22280=CARTESIAN_POINT('Ctrl Pts',(13.5252146997001,1.4082827037902E-5,
4.62497680637469));
#22281=CARTESIAN_POINT('Ctrl Pts',(13.1247853002999,3.84888821536311E-6,
4.62495078081483));
#22282=CARTESIAN_POINT('Ctrl Pts',(13.1290505788821,-0.0558403875021823,
4.6249385719914));
#22283=CARTESIAN_POINT('Ctrl Pts',(13.1411872295142,-0.214751600407627,
4.60383286368317));
#22284=CARTESIAN_POINT('Ctrl Pts',(13.1611952521963,-0.449738236712957,
4.47075670902068));
#22285=CARTESIAN_POINT('Ctrl Pts',(13.1848093683461,-0.619294173608025,
4.2008758003961));
#22286=CARTESIAN_POINT('Ctrl Pts',(13.208423484496,-0.64043195068177,3.88285360784221));
#22287=CARTESIAN_POINT('Ctrl Pts',(13.2320376006459,-0.508085752511173,
3.59290636366459));
#22288=CARTESIAN_POINT('Ctrl Pts',(13.2556517167957,-0.253973266794505,
3.40052194335125));
#22289=CARTESIAN_POINT('Ctrl Pts',(13.2792658329456,0.0610056803032868,
3.3518066124833));
#22290=CARTESIAN_POINT('Ctrl Pts',(13.3028799490955,0.361364191435218,3.45843533922715));
#22291=CARTESIAN_POINT('Ctrl Pts',(13.3264940652453,0.575119258511334,3.69485380694));
#22292=CARTESIAN_POINT('Ctrl Pts',(13.3501081813952,0.65104299168552,4.00440268404554));
#22293=CARTESIAN_POINT('Ctrl Pts',(13.3737222975451,0.570939739771795,4.31289642727099));
#22294=CARTESIAN_POINT('Ctrl Pts',(13.3973364136949,0.354006804717113,4.54640236352309));
#22295=CARTESIAN_POINT('Ctrl Pts',(13.4143574146132,0.136489422610972,4.62032507485564));
#22296=CARTESIAN_POINT('Ctrl Pts',(13.4235070434815,0.0167440814458925,
4.62503846613771));
#22297=CARTESIAN_POINT('Ctrl Pts',(13.4247853002999,1.36962628664097E-5,
4.62502243215823));
#22298=CARTESIAN_POINT('Origin',(11.8752146997001,0.,4.));
#22299=CARTESIAN_POINT('',(12.8247853002999,-1.55438223423121E-5,4.62499607812274));
#22300=CARTESIAN_POINT('',(12.9252146997001,-9.4222586321007E-6,4.62504029123831));
#22301=CARTESIAN_POINT('',(11.8752146997001,-1.68747709936658E-14,4.625));
#22302=CARTESIAN_POINT('Ctrl Pts',(12.9252146997001,-9.42225863212465E-6,
4.62504029123832));
#22303=CARTESIAN_POINT('Ctrl Pts',(12.9259769045375,-0.00998466834883174,
4.6250476064301));
#22304=CARTESIAN_POINT('Ctrl Pts',(12.9346104814248,-0.122971475467856,
4.62239759066569));
#22305=CARTESIAN_POINT('Ctrl Pts',(12.9511154303622,-0.336107011072318,
4.55759164674784));
#22306=CARTESIAN_POINT('Ctrl Pts',(12.974729546512,-0.56049590900091,4.33124115596169));
#22307=CARTESIAN_POINT('Ctrl Pts',(12.9983436626619,-0.650558060547343,
4.02550641626558));
#22308=CARTESIAN_POINT('Ctrl Pts',(13.0219577788117,-0.584709444123524,
3.71365888635357));
#22309=CARTESIAN_POINT('Ctrl Pts',(13.0455718949616,-0.378731139057797,
3.47043499764384));
#22310=CARTESIAN_POINT('Ctrl Pts',(13.0691860111115,-0.0819872800401352,
3.35412504823007));
#22311=CARTESIAN_POINT('Ctrl Pts',(13.0928001272613,0.234405401379786,3.39260352716186));
#22312=CARTESIAN_POINT('Ctrl Pts',(13.1164142434112,0.494621196584012,3.57664879910166));
#22313=CARTESIAN_POINT('Ctrl Pts',(13.1400283595611,0.636297578801308,3.86215313342763));
#22314=CARTESIAN_POINT('Ctrl Pts',(13.1636424757109,0.625480816776257,4.18069342892634));
#22315=CARTESIAN_POINT('Ctrl Pts',(13.1872565918608,0.464763222827219,4.45592928631477));
#22316=CARTESIAN_POINT('Ctrl Pts',(13.2077806665239,0.228267895462889,4.60018049807294));
#22317=CARTESIAN_POINT('Ctrl Pts',(13.220433369137,0.0625891701764018,4.62492503806923));
#22318=CARTESIAN_POINT('Ctrl Pts',(13.2252146997001,-9.32440196474427E-6,
4.62495874418382));
#22319=CARTESIAN_POINT('Ctrl Pts',(12.8247853002999,-1.55438223423052E-5,
4.62499607812274));
#22320=CARTESIAN_POINT('Ctrl Pts',(12.8267227422326,-0.0253767156259869,
4.62502109614712));
#22321=CARTESIAN_POINT('Ctrl Pts',(12.8365315562153,-0.153759343851268,
4.61735081595804));
#22322=CARTESIAN_POINT('Ctrl Pts',(12.854211742248,-0.376327535803878,4.5312757721487));
#22323=CARTESIAN_POINT('Ctrl Pts',(12.8778258583979,-0.583405888470749,
4.28898776831928));
#22324=CARTESIAN_POINT('Ctrl Pts',(12.9014399745477,-0.650666957548692,
3.97744183415536));
#22325=CARTESIAN_POINT('Ctrl Pts',(12.9250540906976,-0.561991161265395,
3.67130212143154));
#22326=CARTESIAN_POINT('Ctrl Pts',(12.9486682068475,-0.338630270727757,
3.44393714350224));
#22327=CARTESIAN_POINT('Ctrl Pts',(12.9722823229973,-0.0341142786054444,
3.34983650006563));
#22328=CARTESIAN_POINT('Ctrl Pts',(12.9958964391472,0.278577437919422,3.41155206540036));
#22329=CARTESIAN_POINT('Ctrl Pts',(13.0195105552971,0.524506132150044,3.61429327464512));
#22330=CARTESIAN_POINT('Ctrl Pts',(13.0431246714469,0.644733280558021,3.90947178565704));
#22331=CARTESIAN_POINT('Ctrl Pts',(13.0667387875968,0.61044561006836,4.22634601343335));
#22332=CARTESIAN_POINT('Ctrl Pts',(13.0903529037467,0.429860399609997,4.4889748434194));
#22333=CARTESIAN_POINT('Ctrl Pts',(13.1097017413144,0.197481915229314,4.60814700801091));
#22334=CARTESIAN_POINT('Ctrl Pts',(13.1211792068321,0.0472175377905832,
4.6249611028038));
#22335=CARTESIAN_POINT('Ctrl Pts',(13.1247853002999,3.84888821536311E-6,
4.62495078081483));
#22336=CARTESIAN_POINT('Origin',(11.8752146997001,0.,4.));
#22337=CARTESIAN_POINT('',(12.5247853002999,3.80998376854277E-6,4.62503871776264));
#22338=CARTESIAN_POINT('',(12.6252146997001,1.49489494596481E-5,4.6250110476872));
#22339=CARTESIAN_POINT('',(11.8752146997001,-1.68747709936658E-14,4.625));
#22340=CARTESIAN_POINT('',(12.5,0.310062960217711,4.54266560670548));
#22341=CARTESIAN_POINT('Ctrl Pts',(12.5,0.310062960217722,4.54266560670548));
#22342=CARTESIAN_POINT('Ctrl Pts',(12.50787137205,0.220600394030941,4.59378185169648));
#22343=CARTESIAN_POINT('Ctrl Pts',(12.5161331388166,0.113220056708515,4.6237347594226));
#22344=CARTESIAN_POINT('Ctrl Pts',(12.5243949055832,0.00511234815255113,
4.6250406321328));
#22345=CARTESIAN_POINT('Ctrl Pts',(12.5247853002999,3.80998376856706E-6,
4.62503871776264));
#22346=CARTESIAN_POINT('',(12.5,0.310062960217774,3.45733439329455));
#22347=CARTESIAN_POINT('Origin',(12.5,0.,4.));
#22348=CARTESIAN_POINT('Ctrl Pts',(12.5,0.310093463203755,3.45730861053195));
#22349=CARTESIAN_POINT('Ctrl Pts',(12.5008157411716,0.319367492808711,3.46259780682489));
#22350=CARTESIAN_POINT('Ctrl Pts',(12.5095028543931,0.416666480413896,3.52147574364868));
#22351=CARTESIAN_POINT('Ctrl Pts',(12.5260613396645,0.569511032758309,3.68451895614546));
#22352=CARTESIAN_POINT('Ctrl Pts',(12.5496754558144,0.651018771792273,3.99264764559437));
#22353=CARTESIAN_POINT('Ctrl Pts',(12.5732895719643,0.576495013506714,4.3025367374363));
#22354=CARTESIAN_POINT('Ctrl Pts',(12.5969036881141,0.363815091701307,4.53992168461618));
#22355=CARTESIAN_POINT('Ctrl Pts',(12.6142120640261,0.144017971622128,4.61907377583531));
#22356=CARTESIAN_POINT('Ctrl Pts',(12.6236490678881,0.0205077016108913,
4.62503160004571));
#22357=CARTESIAN_POINT('Ctrl Pts',(12.6252146997001,1.49489494596471E-5,
4.6250110476872));
#22358=CARTESIAN_POINT('Origin',(11.8752146997001,0.,4.));
#22359=CARTESIAN_POINT('Ctrl Pts',(12.6252146997001,1.49489494596471E-5,
4.6250110476872));
#22360=CARTESIAN_POINT('Ctrl Pts',(12.631520439938,-0.0825216819810338,
4.62492827098767));
#22361=CARTESIAN_POINT('Ctrl Pts',(12.6456975522259,-0.268159494659544,
4.5879440580038));
#22362=CARTESIAN_POINT('Ctrl Pts',(12.6677460365637,-0.506235857616531,
4.40939182910775));
#22363=CARTESIAN_POINT('Ctrl Pts',(12.6913601527136,-0.639894509617229,
4.12004729681268));
#22364=CARTESIAN_POINT('Ctrl Pts',(12.7149742688635,-0.620198095551099,
3.8019325752266));
#22365=CARTESIAN_POINT('Ctrl Pts',(12.7385883850133,-0.451866840211785,
3.53128609963859));
#22366=CARTESIAN_POINT('Ctrl Pts',(12.7622025011632,-0.17524257447904,3.37297016902465));
#22367=CARTESIAN_POINT('Ctrl Pts',(12.7858166173131,0.143379805101228,3.36492630429559));
#22368=CARTESIAN_POINT('Ctrl Pts',(12.809430733463,0.42764021116234,3.50908227080648));
#22369=CARTESIAN_POINT('Ctrl Pts',(12.8330448496128,0.609413666055986,3.77089008898231));
#22370=CARTESIAN_POINT('Ctrl Pts',(12.8566589657627,0.645136892431096,4.08760569204938));
#22371=CARTESIAN_POINT('Ctrl Pts',(12.8802730819125,0.526248572038732,4.38332598125533));
#22372=CARTESIAN_POINT('Ctrl Pts',(12.903124993225,0.289149347937084,4.5805996458561));
#22373=CARTESIAN_POINT('Ctrl Pts',(12.9181055324875,0.0930307802739178,
4.62497206165088));
#22374=CARTESIAN_POINT('Ctrl Pts',(12.9252146997001,-9.42225863212465E-6,
4.62504029123832));
#22375=CARTESIAN_POINT('Ctrl Pts',(12.5247853002999,3.80998376856706E-6,
4.62503871776264));
#22376=CARTESIAN_POINT('Ctrl Pts',(12.5322662776332,-0.0978890574527522,
4.62500203345524));
#22377=CARTESIAN_POINT('Ctrl Pts',(12.5476186270164,-0.298862923743373,
4.57698368148067));
#22378=CARTESIAN_POINT('Ctrl Pts',(12.5708423484496,-0.535054221536356,
4.37092866956447));
#22379=CARTESIAN_POINT('Ctrl Pts',(12.5944564645995,-0.647009713430093,
4.07251155115386));
#22380=CARTESIAN_POINT('Ctrl Pts',(12.6180705807493,-0.603894380709874,
3.75671714932517));
#22381=CARTESIAN_POINT('Ctrl Pts',(12.6416846968992,-0.416056506175611,
3.49922677321964));
#22382=CARTESIAN_POINT('Ctrl Pts',(12.6652988130491,-0.128505496873939,
3.36175035317655));
#22383=CARTESIAN_POINT('Ctrl Pts',(12.6889129291989,0.189841674427298,3.37723482234205));
#22384=CARTESIAN_POINT('Ctrl Pts',(12.7125270453488,0.462692468193658,3.54196933898577));
#22385=CARTESIAN_POINT('Ctrl Pts',(12.7361411614987,0.624655556881011,3.81647407445394));
#22386=CARTESIAN_POINT('Ctrl Pts',(12.7597552776485,0.636915702199809,4.13496208375113));
#22387=CARTESIAN_POINT('Ctrl Pts',(12.7833693937984,0.496534514683115,4.42110548633398));
#22388=CARTESIAN_POINT('Ctrl Pts',(12.8050460680155,0.258436396781676,4.5911312751119));
#22389=CARTESIAN_POINT('Ctrl Pts',(12.8188513701827,0.0776597756952025,
4.62491945378327));
#22390=CARTESIAN_POINT('Ctrl Pts',(12.8247853002999,-1.55438223423052E-5,
4.62499607812274));
#22391=CARTESIAN_POINT('Ctrl Pts',(12.5,-0.186196943290592,3.58169363627332));
#22392=CARTESIAN_POINT('Ctrl Pts',(12.50787137205,-0.117235947257613,3.55099764935784));
#22393=CARTESIAN_POINT('Ctrl Pts',(12.5236141161499,0.0360970477778841,
3.52440632583991));
#22394=CARTESIAN_POINT('Ctrl Pts',(12.5472282322997,0.257537368848111,3.59853698535937));
#22395=CARTESIAN_POINT('Ctrl Pts',(12.5708423484496,0.417223782598737,3.76887858727216));
#22396=CARTESIAN_POINT('Ctrl Pts',(12.5944564645995,0.476936352215019,3.99461366516243));
#22397=CARTESIAN_POINT('Ctrl Pts',(12.6180705807493,0.422340246895018,4.22163841384584));
#22398=CARTESIAN_POINT('Ctrl Pts',(12.6416846968992,0.266530936180377,4.39554662614981));
#22399=CARTESIAN_POINT('Ctrl Pts',(12.6652988130491,0.0468439715927196,
4.47465904879863));
#22400=CARTESIAN_POINT('Ctrl Pts',(12.6889129291989,-0.184068700558194,
4.44001626345752));
#22401=CARTESIAN_POINT('Ctrl Pts',(12.7125270453488,-0.37086838928987,4.29992045400434));
#22402=CARTESIAN_POINT('Ctrl Pts',(12.7361411614987,-0.468786717745582,
4.08794664964497));
#22403=CARTESIAN_POINT('Ctrl Pts',(12.7597552776485,-0.454357124800734,
3.85489580461101));
#22404=CARTESIAN_POINT('Ctrl Pts',(12.7833693937984,-0.331037647139153,
3.65662019659523));
#22405=CARTESIAN_POINT('Ctrl Pts',(12.8069835099483,-0.128382710063344,
3.54063794582746));
#22406=CARTESIAN_POINT('Ctrl Pts',(12.8305976260981,0.10504004521716,3.53474501052695));
#22407=CARTESIAN_POINT('Ctrl Pts',(12.854211742248,0.31328921869753,3.64035367159283));
#22408=CARTESIAN_POINT('Ctrl Pts',(12.8778258583979,0.446456451752615,3.83215407918844));
#22409=CARTESIAN_POINT('Ctrl Pts',(12.9014399745477,0.47262728739502,4.06417992999538));
#22410=CARTESIAN_POINT('Ctrl Pts',(12.9250540906976,0.385529703875575,4.28082461386765));
#22411=CARTESIAN_POINT('Ctrl Pts',(12.9486682068475,0.206037242841946,4.43016772408018));
#22412=CARTESIAN_POINT('Ctrl Pts',(12.9722823229973,-0.0228334776507366,
4.47641814468844));
#22413=CARTESIAN_POINT('Ctrl Pts',(12.9958964391472,-0.24623199631158,4.40849164040747));
#22414=CARTESIAN_POINT('Ctrl Pts',(13.0195105552971,-0.410619302934066,
4.24266727085754));
#22415=CARTESIAN_POINT('Ctrl Pts',(13.0431246714469,-0.476598835156983,
4.01868600055616));
#22416=CARTESIAN_POINT('Ctrl Pts',(13.0667387875968,-0.428358138764893,
3.79022650014263));
#22417=CARTESIAN_POINT('Ctrl Pts',(13.0903529037467,-0.277458432473742,
3.61204067927388));
#22418=CARTESIAN_POINT('Ctrl Pts',(13.1139670198965,-0.060063881357403,
3.52683201033335));
#22419=CARTESIAN_POINT('Ctrl Pts',(13.1375811360464,0.171725397050831,3.55502134399878));
#22420=CARTESIAN_POINT('Ctrl Pts',(13.1611952521963,0.362359488617447,3.68985291022187));
#22421=CARTESIAN_POINT('Ctrl Pts',(13.1848093683461,0.466151606229838,3.89901338554908));
#22422=CARTESIAN_POINT('Ctrl Pts',(13.208423484496,0.458227246370285,4.13237600603144));
#22423=CARTESIAN_POINT('Ctrl Pts',(13.2320376006459,0.34048553704322,4.3340137951542));
#22424=CARTESIAN_POINT('Ctrl Pts',(13.2556517167957,0.141144098528766,4.45560285308526));
#22425=CARTESIAN_POINT('Ctrl Pts',(13.2792658329456,-0.0920235057499227,
4.46800351566886));
#22426=CARTESIAN_POINT('Ctrl Pts',(13.3028799490955,-0.30313703626889,4.36824387779166));
#22427=CARTESIAN_POINT('Ctrl Pts',(13.3264940652453,-0.441601665806575,
4.18023203113149));
#22428=CARTESIAN_POINT('Ctrl Pts',(13.3501081813952,-0.47423338199515,3.94902632355453));
#22429=CARTESIAN_POINT('Ctrl Pts',(13.3737222975451,-0.393211766889608,
3.73003681238273));
#22430=CARTESIAN_POINT('Ctrl Pts',(13.3973364136949,-0.217954214568861,
3.57574585842847));
#22431=CARTESIAN_POINT('Ctrl Pts',(13.4209505298448,0.00953758252632317,
3.52313036287841));
#22432=CARTESIAN_POINT('Ctrl Pts',(13.4445646459947,0.234743631574736,3.58479999551538));
#22433=CARTESIAN_POINT('Ctrl Pts',(13.4681787621445,0.403691735186444,3.74597519957476));
#22434=CARTESIAN_POINT('Ctrl Pts',(13.4917928782944,0.475892304226004,3.96802921540861));
#22435=CARTESIAN_POINT('Ctrl Pts',(13.5154069944443,0.434041969710506,4.19774525232923));
#22436=CARTESIAN_POINT('Ctrl Pts',(13.5390211105941,0.288170455640921,4.38007026295756));
#22437=CARTESIAN_POINT('Ctrl Pts',(13.562635226744,0.0732368858249759,4.47130878927046));
#22438=CARTESIAN_POINT('Ctrl Pts',(13.5862493428939,-0.159248413505658,
4.44959488329479));
#22439=CARTESIAN_POINT('Ctrl Pts',(13.6098634590437,-0.353568721957589,
4.32013243375547));
#22440=CARTESIAN_POINT('Ctrl Pts',(13.6334775751936,-0.46315382488092,4.1139480179165));
#22441=CARTESIAN_POINT('Ctrl Pts',(13.6570916913435,-0.461740889501104,
3.88045516635315));
#22442=CARTESIAN_POINT('Ctrl Pts',(13.6807058074933,-0.349668535617837,
3.67561206636528));
#22443=CARTESIAN_POINT('Ctrl Pts',(13.7043199236432,-0.153795683012805,
3.5485107928471));
#22444=CARTESIAN_POINT('Ctrl Pts',(13.7279340397931,0.0789353756500159,
3.5296120507922));
#22445=CARTESIAN_POINT('Ctrl Pts',(13.7515481559429,0.292749022042461,3.62344505529457));
#22446=CARTESIAN_POINT('Ctrl Pts',(13.7751622720928,0.436403327377467,3.80752207362193));
#22447=CARTESIAN_POINT('Ctrl Pts',(13.7987763882427,0.475470537355291,4.03772776690975));
#22448=CARTESIAN_POINT('Ctrl Pts',(13.8223905043925,0.400587923144683,4.25889173822189));
#22449=CARTESIAN_POINT('Ctrl Pts',(13.8460046205424,0.229701624524423,4.41801050223621));
#22450=CARTESIAN_POINT('Ctrl Pts',(13.8696187366923,0.00376573255618155,
4.47695013947711));
#22451=CARTESIAN_POINT('Ctrl Pts',(13.8932328528421,-0.223072643433687,
4.42158535558109));
#22452=CARTESIAN_POINT('Ctrl Pts',(13.916846968992,-0.396450107540549,4.26518470642179));
#22453=CARTESIAN_POINT('Ctrl Pts',(13.9404610851419,-0.474815543552022,
4.04523069632808));
#22454=CARTESIAN_POINT('Ctrl Pts',(13.9640752012917,-0.439388129199652,
3.81443683499316));
#22455=CARTESIAN_POINT('Ctrl Pts',(13.9876893174416,-0.298658290955197,
3.62811447792009));
#22456=CARTESIAN_POINT('Ctrl Pts',(14.0113034335915,-0.0863529142219465,
3.53091707503438));
#22457=CARTESIAN_POINT('Ctrl Pts',(14.0349175497413,0.146647539536438,3.54613866056158));
#22458=CARTESIAN_POINT('Ctrl Pts',(14.0585316658912,0.344502889581789,3.6701312755675));
#22459=CARTESIAN_POINT('Ctrl Pts',(14.0821457820411,0.459795723937725,3.87317922671144));
#22460=CARTESIAN_POINT('Ctrl Pts',(14.1057598981909,0.464895312258427,4.10662065901627));
#22461=CARTESIAN_POINT('Ctrl Pts',(14.1293740143408,0.358579502702881,4.31450970816539));
#22462=CARTESIAN_POINT('Ctrl Pts',(14.1529881304907,0.166327619131383,4.44702431634421));
#22463=CARTESIAN_POINT('Ctrl Pts',(14.1766022466405,-0.0657858362277661,
4.47240643522367));
#22464=CARTESIAN_POINT('Ctrl Pts',(14.2002163627904,-0.282133257977474,
4.38457306332079));
#22465=CARTESIAN_POINT('Ctrl Pts',(14.2238304789403,-0.430865480427841,
4.20457407964992));
#22466=CARTESIAN_POINT('Ctrl Pts',(14.2474445950901,-0.476337791093329,
3.97554749368157));
#22467=CARTESIAN_POINT('Ctrl Pts',(14.27105871124,-0.407652434174819,3.75238112107461));
#22468=CARTESIAN_POINT('Ctrl Pts',(14.2946728273899,-0.241270333599833,
3.58855833656088));
#22469=CARTESIAN_POINT('Ctrl Pts',(14.3182869435397,-0.0170661180132474,
3.52334041087493));
#22470=CARTESIAN_POINT('Ctrl Pts',(14.3419010596896,0.211228111558234,3.57235727391142));
#22471=CARTESIAN_POINT('Ctrl Pts',(14.3655151758395,0.388900053764453,3.72386169322071));
#22472=CARTESIAN_POINT('Ctrl Pts',(14.3891292919893,0.473369390821204,3.94154458004181));
#22473=CARTESIAN_POINT('Ctrl Pts',(14.4127434081392,0.444392458083208,4.17323671518384));
#22474=CARTESIAN_POINT('Ctrl Pts',(14.4363575242891,0.308913779199362,4.3634114655727));
#22475=CARTESIAN_POINT('Ctrl Pts',(14.4599716404389,0.0994017626770733,
4.46649212840691));
#22476=CARTESIAN_POINT('Ctrl Pts',(14.4835857565888,-0.133932578240045,
4.45777470525894));
#22477=CARTESIAN_POINT('Ctrl Pts',(14.5071998727387,-0.335169044432007,
4.33934838727104));
#22478=CARTESIAN_POINT('Ctrl Pts',(14.5308139888885,-0.456079915900645,
4.13959486595487));
#22479=CARTESIAN_POINT('Ctrl Pts',(14.5544281050384,-0.467688060597361,
3.90638646324521));
#22480=CARTESIAN_POINT('Ctrl Pts',(14.5780422211883,-0.367211505836647,
3.69561319629505));
#22481=CARTESIAN_POINT('Ctrl Pts',(14.6016563373381,-0.178730157419731,
3.55778834579073));
#22482=CARTESIAN_POINT('Ctrl Pts',(14.625270453488,0.0525851174261518,3.52594259660587));
#22483=CARTESIAN_POINT('Ctrl Pts',(14.6488845696379,0.271298002813252,3.60770800421126));
#22484=CARTESIAN_POINT('Ctrl Pts',(14.6724986857877,0.424992433239313,3.78348891949988));
#22485=CARTESIAN_POINT('Ctrl Pts',(14.6961128019376,0.476834468501385,4.01115822240469));
#22486=CARTESIAN_POINT('Ctrl Pts',(14.7197269180875,0.414399804028447,4.23615337970372));
#22487=CARTESIAN_POINT('Ctrl Pts',(14.7433410342373,0.252651341641402,4.40455273546398));
#22488=CARTESIAN_POINT('Ctrl Pts',(14.7669551503872,0.0303532266559796,
4.47599821226155));
#22489=CARTESIAN_POINT('Ctrl Pts',(14.7905692665371,-0.199219250862459,
4.43336740322118));
#22490=CARTESIAN_POINT('Ctrl Pts',(14.8141833826869,-0.381047447081096,
4.28687708064914));
#22491=CARTESIAN_POINT('Ctrl Pts',(14.8377974988368,-0.471554972144783,
4.07163466550741));
#22492=CARTESIAN_POINT('Ctrl Pts',(14.8614116149867,-0.449051060899263,
3.83922451083896));
#22493=CARTESIAN_POINT('Ctrl Pts',(14.8850257311365,-0.318928946727196,
3.64534530693059));
#22494=CARTESIAN_POINT('Ctrl Pts',(14.9086398472864,-0.112373269271187,
3.53646160000302));
#22495=CARTESIAN_POINT('Ctrl Pts',(14.9322539634362,0.121113399391719,3.5386680312482));
#22496=CARTESIAN_POINT('Ctrl Pts',(14.9558680795861,0.325574495333277,3.65143602219853));
#22497=CARTESIAN_POINT('Ctrl Pts',(14.979482195736,0.452009190454857,3.84773949289016));
#22498=CARTESIAN_POINT('Ctrl Pts',(15.0030963118858,0.470117180575255,4.08053390545391));
#22499=CARTESIAN_POINT('Ctrl Pts',(15.0267104280357,0.375557372208547,4.29402641177155));
#22500=CARTESIAN_POINT('Ctrl Pts',(15.0503245441856,0.190994688421392,4.43705643304037));
#22501=CARTESIAN_POINT('Ctrl Pts',(15.0739386603355,-0.0393454023191647,
4.47533644032795));
#22502=CARTESIAN_POINT('Ctrl Pts',(15.0975527764853,-0.260245916509526,
4.39971253597763));
#22503=CARTESIAN_POINT('Ctrl Pts',(15.1211668926352,-0.418792603204267,
4.22826540530875));
#22504=CARTESIAN_POINT('Ctrl Pts',(15.1369096367351,-0.457530945318996,
4.07754232577813));
#22505=CARTESIAN_POINT('Ctrl Pts',(15.1447810087851,-0.457870370902723,
4.00205890126089));
#22506=CARTESIAN_POINT('Ctrl Pts',(12.4850729970717,-0.208850989443975,
3.53079950502365));
#22507=CARTESIAN_POINT('Ctrl Pts',(12.4929443691216,-0.131499707516366,
3.49636882573344));
#22508=CARTESIAN_POINT('Ctrl Pts',(12.5086871132215,0.0404888716816997,
3.46654221242176));
#22509=CARTESIAN_POINT('Ctrl Pts',(12.5323012293714,0.288871199237585,3.54969213591223));
#22510=CARTESIAN_POINT('Ctrl Pts',(12.5559153455212,0.467986199318594,3.74075871022993));
#22511=CARTESIAN_POINT('Ctrl Pts',(12.5795294616711,0.534963825407437,3.99395832530641));
#22512=CARTESIAN_POINT('Ctrl Pts',(12.603143577821,0.473725169098917,4.24860452170932));
#22513=CARTESIAN_POINT('Ctrl Pts',(12.6267576939708,0.298958988020687,4.4436716456386));
#22514=CARTESIAN_POINT('Ctrl Pts',(12.6503718101207,0.0525433427838623,
4.53240944903922));
#22515=CARTESIAN_POINT('Ctrl Pts',(12.6739859262706,-0.206463809544117,
4.49355177571912));
#22516=CARTESIAN_POINT('Ctrl Pts',(12.6976000424205,-0.41599087873209,4.33641091237214));
#22517=CARTESIAN_POINT('Ctrl Pts',(12.7212141585703,-0.525822648369464,
4.09864686536754));
#22518=CARTESIAN_POINT('Ctrl Pts',(12.7448282747202,-0.509637448384189,
3.8372413948162));
#22519=CARTESIAN_POINT('Ctrl Pts',(12.76844239087,-0.37131404483003,3.61484216427635));
#22520=CARTESIAN_POINT('Ctrl Pts',(12.7920565070199,-0.144002664868576,
3.48474868689319));
#22521=CARTESIAN_POINT('Ctrl Pts',(12.8156706231698,0.117819965178516,3.47813877511649));
#22522=CARTESIAN_POINT('Ctrl Pts',(12.8392847393197,0.351406216185799,3.59659653799738));
#22523=CARTESIAN_POINT('Ctrl Pts',(12.8628988554695,0.500775523187073,3.81173274911973));
#22524=CARTESIAN_POINT('Ctrl Pts',(12.8865129716194,0.530130489073712,4.07198851734671));
#22525=CARTESIAN_POINT('Ctrl Pts',(12.9101270877692,0.432435993263294,4.31499173633021));
#22526=CARTESIAN_POINT('Ctrl Pts',(12.9337412039191,0.231105201134755,4.48250499290311));
#22527=CARTESIAN_POINT('Ctrl Pts',(12.957355320069,-0.0256115611541523,
4.53438256906268));
#22528=CARTESIAN_POINT('Ctrl Pts',(12.9809694362189,-0.276190334565159,
4.45819164252092));
#22529=CARTESIAN_POINT('Ctrl Pts',(13.0045835523687,-0.460578171623014,
4.27219189922559));
#22530=CARTESIAN_POINT('Ctrl Pts',(13.0281976685186,-0.534585243620437,
4.0209594724593));
#22531=CARTESIAN_POINT('Ctrl Pts',(13.0518117846684,-0.480475240551103,
3.76470396221295));
#22532=CARTESIAN_POINT('Ctrl Pts',(13.0754259008183,-0.311216001335094,
3.5648387853972));
#22533=CARTESIAN_POINT('Ctrl Pts',(13.0990400169682,-0.0673716809183137,
3.46926302296559));
#22534=CARTESIAN_POINT('Ctrl Pts',(13.122654133118,0.19261873182715,3.50088207171981));
#22535=CARTESIAN_POINT('Ctrl Pts',(13.1462682492679,0.406446724606302,3.65211820651514));
#22536=CARTESIAN_POINT('Ctrl Pts',(13.1698823654178,0.522866930420328,3.88672663484193));
#22537=CARTESIAN_POINT('Ctrl Pts',(13.1934964815676,0.513978436505609,4.14848181366307));
#22538=CARTESIAN_POINT('Ctrl Pts',(13.2171105977175,0.381911432304553,4.37465229220773));
#22539=CARTESIAN_POINT('Ctrl Pts',(13.2407247138674,0.158316694737061,4.51103474084347));
#22540=CARTESIAN_POINT('Ctrl Pts',(13.2643388300172,-0.103219740820234,
4.52494415635039));
#22541=CARTESIAN_POINT('Ctrl Pts',(13.2879529461671,-0.340018846942428,
4.41304705047411));
#22542=CARTESIAN_POINT('Ctrl Pts',(13.311567062317,-0.495330069408668,4.20216034359148));
#22543=CARTESIAN_POINT('Ctrl Pts',(13.3351811784669,-0.531931992580964,
3.94282450306062));
#22544=CARTESIAN_POINT('Ctrl Pts',(13.3587952946167,-0.44105271077271,3.69719116838925));
#22545=CARTESIAN_POINT('Ctrl Pts',(13.3824094107666,-0.244472076510672,
3.5241280781681));
#22546=CARTESIAN_POINT('Ctrl Pts',(13.4060235269164,0.0106979927399635,
3.46511100671938));
#22547=CARTESIAN_POINT('Ctrl Pts',(13.4296376430663,0.263304213558122,3.53428380605355));
#22548=CARTESIAN_POINT('Ctrl Pts',(13.4532517592162,0.452807746647384,3.71506873327496));
#22549=CARTESIAN_POINT('Ctrl Pts',(13.476865875366,0.533792751104717,3.96413942206993));
#22550=CARTESIAN_POINT('Ctrl Pts',(13.5004799915159,0.486850606847911,4.22180434800346));
#22551=CARTESIAN_POINT('Ctrl Pts',(13.5240941076658,0.323231325528255,4.42631231788287));
#22552=CARTESIAN_POINT('Ctrl Pts',(13.5477082238157,0.0821474069231642,
4.52865157307741));
#22553=CARTESIAN_POINT('Ctrl Pts',(13.5713223399655,-0.178623709606947,
4.50429579866153));
#22554=CARTESIAN_POINT('Ctrl Pts',(13.5949364561154,-0.396586410669692,
4.35908202552279));
#22555=CARTESIAN_POINT('Ctrl Pts',(13.6185505722652,-0.519504417643299,
4.12781174527607));
#22556=CARTESIAN_POINT('Ctrl Pts',(13.6421646884151,-0.517919574482721,
3.86591049053316));
#22557=CARTESIAN_POINT('Ctrl Pts',(13.665778804565,-0.392211699884016,3.6361447201764));
#22558=CARTESIAN_POINT('Ctrl Pts',(13.6893929207148,-0.172507561089802,
3.49357940054904));
#22559=CARTESIAN_POINT('Ctrl Pts',(13.7130070368647,0.0885392156030666,
3.47238130294519));
#22560=CARTESIAN_POINT('Ctrl Pts',(13.7366211530146,0.328366952925232,3.57763069902274));
#22561=CARTESIAN_POINT('Ctrl Pts',(13.7602352691644,0.489499264105438,3.78410383833506));
#22562=CARTESIAN_POINT('Ctrl Pts',(13.7838493853143,0.533319669072828,4.04231799571659));
#22563=CARTESIAN_POINT('Ctrl Pts',(13.8074635014642,0.449326302728307,4.29039035083475));
#22564=CARTESIAN_POINT('Ctrl Pts',(13.831077617614,0.257648760022572,4.46886863686992));
#22565=CARTESIAN_POINT('Ctrl Pts',(13.8546917337639,0.00422389839726028,
4.53497929012603));
#22566=CARTESIAN_POINT('Ctrl Pts',(13.8783058499138,-0.25021324988294,4.47287843233165));
#22567=CARTESIAN_POINT('Ctrl Pts',(13.9019199660636,-0.444685051009628,
4.29744896636227));
#22568=CARTESIAN_POINT('Ctrl Pts',(13.9255340822135,-0.532584984058807,
4.05073378496132));
#22569=CARTESIAN_POINT('Ctrl Pts',(13.9491481983634,-0.492847218174075,
3.79185989881933));
#22570=CARTESIAN_POINT('Ctrl Pts',(13.9727623145132,-0.334995185577738,
3.58286823685896));
#22571=CARTESIAN_POINT('Ctrl Pts',(13.9963764306631,-0.0968592247428986,
3.47384510573062));
#22572=CARTESIAN_POINT('Ctrl Pts',(14.019990546813,0.164489723571401,3.49091865775613));
#22573=CARTESIAN_POINT('Ctrl Pts',(14.0436046629628,0.386417564563212,3.62999709733779));
#22574=CARTESIAN_POINT('Ctrl Pts',(14.0672187791127,0.515737746224078,3.85774930825782));
#22575=CARTESIAN_POINT('Ctrl Pts',(14.0908328952626,0.521457786777448,4.11959288770904));
#22576=CARTESIAN_POINT('Ctrl Pts',(14.1144470114124,0.402206838685568,4.35277519909424));
#22577=CARTESIAN_POINT('Ctrl Pts',(14.1380611275623,0.186564221804844,4.50141247822903));
#22578=CARTESIAN_POINT('Ctrl Pts',(14.1616752437122,-0.0737898095680628,
4.52988276645436));
#22579=CARTESIAN_POINT('Ctrl Pts',(14.185289359862,-0.316459599402161,4.43136296100575));
#22580=CARTESIAN_POINT('Ctrl Pts',(14.2089034760119,-0.483287643257218,
4.22946401908862));
#22581=CARTESIAN_POINT('Ctrl Pts',(14.2325175921618,-0.53429243907693,3.97257242762026));
#22582=CARTESIAN_POINT('Ctrl Pts',(14.2561317083116,-0.457250332481466,
3.72225404480531));
#22583=CARTESIAN_POINT('Ctrl Pts',(14.2797458244615,-0.270625000632592,
3.53849941363631));
#22584=CARTESIAN_POINT('Ctrl Pts',(14.3033599406114,-0.0191425034699505,
3.46534661065105));
#22585=CARTESIAN_POINT('Ctrl Pts',(14.3269740567612,0.236927627906706,3.52032721432634));
#22586=CARTESIAN_POINT('Ctrl Pts',(14.3505881729111,0.436216403922163,3.69026474025285));
#22587=CARTESIAN_POINT('Ctrl Pts',(14.374202289061,0.530962882087739,3.93443247734966));
#22588=CARTESIAN_POINT('Ctrl Pts',(14.3978164052108,0.498460409348769,4.19431392768733));
#22589=CARTESIAN_POINT('Ctrl Pts',(14.4214305213607,0.346498429557861,4.40762669256976));
#22590=CARTESIAN_POINT('Ctrl Pts',(14.4450446375106,0.111495689030631,4.52324888295055));
#22591=CARTESIAN_POINT('Ctrl Pts',(14.4686587536604,-0.150227769531968,
4.51347083601981));
#22592=CARTESIAN_POINT('Ctrl Pts',(14.4922728698103,-0.375948097339969,
4.38063592879268));
#22593=CARTESIAN_POINT('Ctrl Pts',(14.5158869859602,-0.51156984651846,4.15657897149511));
#22594=CARTESIAN_POINT('Ctrl Pts',(14.53950110211,-0.52459032076832,3.89499677367918));
#22595=CARTESIAN_POINT('Ctrl Pts',(14.5631152182599,-0.411889072794842,
3.65857933001481));
#22596=CARTESIAN_POINT('Ctrl Pts',(14.5867293344098,-0.200475741228102,
3.50398572665543));
#22597=CARTESIAN_POINT('Ctrl Pts',(14.6103434505596,0.0589829973059192,
3.46826539682992));
#22598=CARTESIAN_POINT('Ctrl Pts',(14.6339575667095,0.304306049929579,3.5599789662306));
#22599=CARTESIAN_POINT('Ctrl Pts',(14.6575716828594,0.476700039321847,3.75714663952638));
#22600=CARTESIAN_POINT('Ctrl Pts',(14.6811857990092,0.53484954579562,4.0125158112076));
#22601=CARTESIAN_POINT('Ctrl Pts',(14.7047999151591,0.464818635404008,4.26488548168423));
#22602=CARTESIAN_POINT('Ctrl Pts',(14.728414031309,0.283390703164248,4.45377350235044));
#22603=CARTESIAN_POINT('Ctrl Pts',(14.7520281474588,0.0340462163765225,
4.5339115446661));
#22604=CARTESIAN_POINT('Ctrl Pts',(14.7756422636087,-0.223457683695575,
4.48609396779546));
#22605=CARTESIAN_POINT('Ctrl Pts',(14.7992563797586,-0.427408393186059,
4.32178058932398));
#22606=CARTESIAN_POINT('Ctrl Pts',(14.8228704959084,-0.528927708313459,
4.08035024907128));
#22607=CARTESIAN_POINT('Ctrl Pts',(14.8464846120583,-0.503685810960444,
3.81966341983811));
#22608=CARTESIAN_POINT('Ctrl Pts',(14.8700987282082,-0.357732113691821,
3.6021954912391));
#22609=CARTESIAN_POINT('Ctrl Pts',(14.893712844358,-0.126045401495737,3.48006421709321));
#22610=CARTESIAN_POINT('Ctrl Pts',(14.9173269605079,0.13584891809103,3.48253909847714));
#22611=CARTESIAN_POINT('Ctrl Pts',(14.9409410766578,0.365186207068703,3.60902724630258));
#22612=CARTESIAN_POINT('Ctrl Pts',(14.9645551928076,0.507003847624586,3.82921439524653));
#22613=CARTESIAN_POINT('Ctrl Pts',(14.9881693089575,0.52731498478211,4.0903322339271));
#22614=CARTESIAN_POINT('Ctrl Pts',(15.0117834251074,0.421250356706029,4.32979975898591));
#22615=CARTESIAN_POINT('Ctrl Pts',(15.0353975412572,0.214232462415332,4.49023183125449));
#22616=CARTESIAN_POINT('Ctrl Pts',(15.0590116574071,-0.0441324441701724,
4.53316925684615));
#22617=CARTESIAN_POINT('Ctrl Pts',(15.082625773557,-0.291909288096862,4.4483444097243));
#22618=CARTESIAN_POINT('Ctrl Pts',(15.1062398897068,-0.469745893811612,
4.25603780014884));
#22619=CARTESIAN_POINT('Ctrl Pts',(15.1219826338067,-0.513197418509596,
4.08697667736293));
#22620=CARTESIAN_POINT('Ctrl Pts',(15.1298540058567,-0.513578141027115,
4.0023094018511));
#22621=CARTESIAN_POINT('Ctrl Pts',(12.4701459941433,-0.231505035597357,
3.47990537377399));
#22622=CARTESIAN_POINT('Ctrl Pts',(12.4780173661933,-0.145763467775118,
3.44174000210903));
#22623=CARTESIAN_POINT('Ctrl Pts',(12.4937601102932,0.0448806955855158,
3.40867809900361));
#22624=CARTESIAN_POINT('Ctrl Pts',(12.517374226443,0.320205029627059,3.5008472864651));
#22625=CARTESIAN_POINT('Ctrl Pts',(12.5409883425929,0.518748616038451,3.71263883318769));
#22626=CARTESIAN_POINT('Ctrl Pts',(12.5646024587428,0.592991298599855,3.99330298545039));
#22627=CARTESIAN_POINT('Ctrl Pts',(12.5882165748926,0.525110091302815,4.27557062957281));
#22628=CARTESIAN_POINT('Ctrl Pts',(12.6118306910425,0.331387039860997,4.49179666512739));
#22629=CARTESIAN_POINT('Ctrl Pts',(12.6354448071924,0.0582427139750047,
4.5901598492798));
#22630=CARTESIAN_POINT('Ctrl Pts',(12.6590589233422,-0.22885891853004,4.54708728798072));
#22631=CARTESIAN_POINT('Ctrl Pts',(12.6826730394921,-0.461113368174311,
4.37290137073994));
#22632=CARTESIAN_POINT('Ctrl Pts',(12.706287155642,-0.582858578993347,4.10934708109011));
#22633=CARTESIAN_POINT('Ctrl Pts',(12.7299012717918,-0.564917771967644,
3.8195869850214));
#22634=CARTESIAN_POINT('Ctrl Pts',(12.7535153879417,-0.411590442520908,
3.57306413195747));
#22635=CARTESIAN_POINT('Ctrl Pts',(12.7771295040916,-0.159622619673808,
3.42885942795892));
#22636=CARTESIAN_POINT('Ctrl Pts',(12.8007436202414,0.130599885139872,3.42153253970604));
#22637=CARTESIAN_POINT('Ctrl Pts',(12.8243577363913,0.38952321367407,3.55283940440193));
#22638=CARTESIAN_POINT('Ctrl Pts',(12.8479718525412,0.555094594621529,3.79131141905102));
#22639=CARTESIAN_POINT('Ctrl Pts',(12.871585968691,0.587633690752404,4.07979710469805));
#22640=CARTESIAN_POINT('Ctrl Pts',(12.8952000848409,0.479342282651013,4.34915885879276));
#22641=CARTESIAN_POINT('Ctrl Pts',(12.9188142009908,0.256173159427565,4.53484226172604));
#22642=CARTESIAN_POINT('Ctrl Pts',(12.9424283171406,-0.0283896446575681,
4.59234699343691));
#22643=CARTESIAN_POINT('Ctrl Pts',(12.9660424332905,-0.306148672818738,
4.50789164463438));
#22644=CARTESIAN_POINT('Ctrl Pts',(12.9896565494404,-0.510537040311962,
4.30171652759364));
#22645=CARTESIAN_POINT('Ctrl Pts',(13.0132706655902,-0.59257165208389,4.02323294436244));
#22646=CARTESIAN_POINT('Ctrl Pts',(13.0368847817401,-0.532592342337314,
3.73918142428326));
#22647=CARTESIAN_POINT('Ctrl Pts',(13.06049889789,-0.344973570196446,3.51763689152052));
#22648=CARTESIAN_POINT('Ctrl Pts',(13.0841130140398,-0.0746794804792245,
3.41169403559782));
#22649=CARTESIAN_POINT('Ctrl Pts',(13.1077271301897,0.213512066603468,3.44674279944083));
#22650=CARTESIAN_POINT('Ctrl Pts',(13.1313412463396,0.450533960595157,3.6143835028084));
#22651=CARTESIAN_POINT('Ctrl Pts',(13.1549553624894,0.579582254610818,3.87443988413478));
#22652=CARTESIAN_POINT('Ctrl Pts',(13.1785694786393,0.569729626640933,4.1645876212947));
#22653=CARTESIAN_POINT('Ctrl Pts',(13.2021835947892,0.423337327565886,4.41529078926125));
#22654=CARTESIAN_POINT('Ctrl Pts',(13.225797710939,0.175489290945357,4.56646662860168));
#22655=CARTESIAN_POINT('Ctrl Pts',(13.2494118270889,-0.114415975890545,
4.58188479703192));
#22656=CARTESIAN_POINT('Ctrl Pts',(13.2730259432388,-0.376900657615966,
4.45785022315656));
#22657=CARTESIAN_POINT('Ctrl Pts',(13.2966400593886,-0.54905847301076,4.22408865605146));
#22658=CARTESIAN_POINT('Ctrl Pts',(13.3202541755385,-0.589630603166779,
3.93662268256671));
#22659=CARTESIAN_POINT('Ctrl Pts',(13.3438682916884,-0.488893654655812,
3.66434552439578));
#22660=CARTESIAN_POINT('Ctrl Pts',(13.3674824078382,-0.270989938452484,
3.47251029790774));
#22661=CARTESIAN_POINT('Ctrl Pts',(13.3910965239881,0.0118584029536041,
3.40709165056035));
#22662=CARTESIAN_POINT('Ctrl Pts',(13.414710640138,0.291864795541507,3.48376761659174));
#22663=CARTESIAN_POINT('Ctrl Pts',(13.4383247562878,0.501923758108325,3.68416226697515));
#22664=CARTESIAN_POINT('Ctrl Pts',(13.4619388724377,0.591693197983429,3.96024962873126));
#22665=CARTESIAN_POINT('Ctrl Pts',(13.4855529885876,0.539659243985316,4.2458634436777));
#22666=CARTESIAN_POINT('Ctrl Pts',(13.5091671047374,0.358292195415589,4.47255437280819));
#22667=CARTESIAN_POINT('Ctrl Pts',(13.5327812208873,0.0910579280213527,
4.58599435688436));
#22668=CARTESIAN_POINT('Ctrl Pts',(13.5563953370372,-0.197999005708236,
4.55899671402827));
#22669=CARTESIAN_POINT('Ctrl Pts',(13.580009453187,-0.439604099381795,4.39803161729011));
#22670=CARTESIAN_POINT('Ctrl Pts',(13.6036235693369,-0.575855010405679,
4.14167547263565));
#22671=CARTESIAN_POINT('Ctrl Pts',(13.6272376854868,-0.574098259464336,
3.85136581471317));
#22672=CARTESIAN_POINT('Ctrl Pts',(13.6508518016366,-0.434754864150196,
3.59667737398752));
#22673=CARTESIAN_POINT('Ctrl Pts',(13.6744659177865,-0.191219439166798,
3.43864800825098));
#22674=CARTESIAN_POINT('Ctrl Pts',(13.6980800339364,0.0981430555561168,
3.41515055509818));
#22675=CARTESIAN_POINT('Ctrl Pts',(13.7216941500862,0.363984883808003,3.53181634275091));
#22676=CARTESIAN_POINT('Ctrl Pts',(13.7453082662361,0.54259520083341,3.76068560304818));
#22677=CARTESIAN_POINT('Ctrl Pts',(13.768922382386,0.591168800790367,4.04690822452342));
#22678=CARTESIAN_POINT('Ctrl Pts',(13.7925364985358,0.498064682311931,4.32188896344761));
#22679=CARTESIAN_POINT('Ctrl Pts',(13.8161506146857,0.28559589552072,4.51972677150362));
#22680=CARTESIAN_POINT('Ctrl Pts',(13.8397647308356,0.00468206423833927,
4.59300844077494));
#22681=CARTESIAN_POINT('Ctrl Pts',(13.8633788469854,-0.277353856332193,
4.52417150908221));
#22682=CARTESIAN_POINT('Ctrl Pts',(13.8869929631353,-0.492919994478707,
4.32971322630275));
#22683=CARTESIAN_POINT('Ctrl Pts',(13.9106070792852,-0.590354424565592,
4.05623687359455));
#22684=CARTESIAN_POINT('Ctrl Pts',(13.934221195435,-0.546306307148498,3.76928296264551));
#22685=CARTESIAN_POINT('Ctrl Pts',(13.9578353115849,-0.371332080200278,
3.53762199579782));
#22686=CARTESIAN_POINT('Ctrl Pts',(13.9814494277348,-0.107365535263851,
3.41677313642685));
#22687=CARTESIAN_POINT('Ctrl Pts',(14.0050635438846,0.182331907606365,3.43569865495067));
#22688=CARTESIAN_POINT('Ctrl Pts',(14.0286776600345,0.428332239544634,3.58986291910809));
#22689=CARTESIAN_POINT('Ctrl Pts',(14.0522917761844,0.571679768510432,3.8423193898042));
#22690=CARTESIAN_POINT('Ctrl Pts',(14.0759058923342,0.578020261296468,4.1325651164018));
#22691=CARTESIAN_POINT('Ctrl Pts',(14.0995200084841,0.445834174668256,4.39104069002309));
#22692=CARTESIAN_POINT('Ctrl Pts',(14.123134124634,0.206800824478305,4.55580064011384));
#22693=CARTESIAN_POINT('Ctrl Pts',(14.1467482407838,-0.0817937829083601,
4.58735909768505));
#22694=CARTESIAN_POINT('Ctrl Pts',(14.1703623569337,-0.350785940826847,
4.4781528586907));
#22695=CARTESIAN_POINT('Ctrl Pts',(14.1939764730836,-0.535709806086595,
4.25435395852733));
#22696=CARTESIAN_POINT('Ctrl Pts',(14.2175905892334,-0.59224708706053,3.96959736155895));
#22697=CARTESIAN_POINT('Ctrl Pts',(14.2412047053833,-0.506848230788112,
3.69212696853602));
#22698=CARTESIAN_POINT('Ctrl Pts',(14.2648188215332,-0.29997966766535,3.48844049071174));
#22699=CARTESIAN_POINT('Ctrl Pts',(14.288432937683,-0.0212188889266537,
3.40735281042717));
#22700=CARTESIAN_POINT('Ctrl Pts',(14.3120470538329,0.262627144255178,3.46829715474127));
#22701=CARTESIAN_POINT('Ctrl Pts',(14.3356611699828,0.483532754079872,3.65666778728498));
#22702=CARTESIAN_POINT('Ctrl Pts',(14.3592752861326,0.588556373354274,3.9273203746575));
#22703=CARTESIAN_POINT('Ctrl Pts',(14.3828894022825,0.55252836061433,4.21539114019081));
#22704=CARTESIAN_POINT('Ctrl Pts',(14.4065035184324,0.384083079916361,4.45184191956682));
#22705=CARTESIAN_POINT('Ctrl Pts',(14.4301176345822,0.123589615384189,4.58000563749418));
#22706=CARTESIAN_POINT('Ctrl Pts',(14.4537317507321,-0.166522960823891,
4.56916696678068));
#22707=CARTESIAN_POINT('Ctrl Pts',(14.477345866882,-0.416727150247931,4.42192347031433));
#22708=CARTESIAN_POINT('Ctrl Pts',(14.5009599830318,-0.567059777136274,
4.17356307703535));
#22709=CARTESIAN_POINT('Ctrl Pts',(14.5245740991817,-0.58149258093928,3.88360708411314));
#22710=CARTESIAN_POINT('Ctrl Pts',(14.5481882153316,-0.456566639753037,
3.62154546373458));
#22711=CARTESIAN_POINT('Ctrl Pts',(14.5718023314814,-0.222221325036472,
3.45018310752014));
#22712=CARTESIAN_POINT('Ctrl Pts',(14.5954164476313,0.0653808771856868,
3.41058819705396));
#22713=CARTESIAN_POINT('Ctrl Pts',(14.6190305637812,0.337314097045906,3.51224992824993));
#22714=CARTESIAN_POINT('Ctrl Pts',(14.642644679931,0.528407645404381,3.73080435955289));
#22715=CARTESIAN_POINT('Ctrl Pts',(14.6662587960809,0.592864623089856,4.0138734000105));
#22716=CARTESIAN_POINT('Ctrl Pts',(14.6898729122308,0.515237466779568,4.29361758366474));
#22717=CARTESIAN_POINT('Ctrl Pts',(14.7134870283806,0.314130064687094,4.5029942692369));
#22718=CARTESIAN_POINT('Ctrl Pts',(14.7371011445305,0.0377392060970651,
4.59182487707066));
#22719=CARTESIAN_POINT('Ctrl Pts',(14.7607152606804,-0.24769611652869,4.53882053236973));
#22720=CARTESIAN_POINT('Ctrl Pts',(14.7843293768302,-0.47376933929102,4.35668409799883));
#22721=CARTESIAN_POINT('Ctrl Pts',(14.8079434929801,-0.586300444482135,
4.08906583263515));
#22722=CARTESIAN_POINT('Ctrl Pts',(14.83155760913,-0.558320561021625,3.80010232883727));
#22723=CARTESIAN_POINT('Ctrl Pts',(14.8551717252798,-0.396535280656446,
3.55904567554761));
#22724=CARTESIAN_POINT('Ctrl Pts',(14.8787858414297,-0.139717533720287,
3.42366683418339));
#22725=CARTESIAN_POINT('Ctrl Pts',(14.9023999575795,0.150584436790342,3.42641016570609));
#22726=CARTESIAN_POINT('Ctrl Pts',(14.9260140737294,0.404797918804129,3.56661847040663));
#22727=CARTESIAN_POINT('Ctrl Pts',(14.9496281898793,0.561998504794314,3.8106892976029));
#22728=CARTESIAN_POINT('Ctrl Pts',(14.9732423060292,0.584512788988964,4.10013056240029));
#22729=CARTESIAN_POINT('Ctrl Pts',(14.996856422179,0.466943341203511,4.36557310620026));
#22730=CARTESIAN_POINT('Ctrl Pts',(15.0204705383289,0.237470236409271,4.54340722946861));
#22731=CARTESIAN_POINT('Ctrl Pts',(15.0440846544788,-0.0489194860211801,
4.59100207336435));
#22732=CARTESIAN_POINT('Ctrl Pts',(15.0676987706286,-0.323572659684198,
4.49697628347096));
#22733=CARTESIAN_POINT('Ctrl Pts',(15.0913128867785,-0.520699184418956,
4.28381019498893));
#22734=CARTESIAN_POINT('Ctrl Pts',(15.1070556308784,-0.568863891700195,
4.09641102894772));
#22735=CARTESIAN_POINT('Ctrl Pts',(15.1149270029284,-0.569285911151507,
4.00255990244131));
#22736=CARTESIAN_POINT('Ctrl Pts',(12.455218991215,-0.25415908175074,3.42901124252432));
#22737=CARTESIAN_POINT('Ctrl Pts',(12.4630903632649,-0.16002722803387,3.38711117848463));
#22738=CARTESIAN_POINT('Ctrl Pts',(12.4788331073648,0.0492725194893315,
3.35081398558546));
#22739=CARTESIAN_POINT('Ctrl Pts',(12.5024472235147,0.351538860016532,3.45200243701797));
#22740=CARTESIAN_POINT('Ctrl Pts',(12.5260613396645,0.569511032758309,3.68451895614546));
#22741=CARTESIAN_POINT('Ctrl Pts',(12.5496754558144,0.651018771792273,3.99264764559437));
#22742=CARTESIAN_POINT('Ctrl Pts',(12.5732895719643,0.576495013506714,4.3025367374363));
#22743=CARTESIAN_POINT('Ctrl Pts',(12.5969036881141,0.363815091701307,4.53992168461618));
#22744=CARTESIAN_POINT('Ctrl Pts',(12.620517804264,0.0639420851661475,4.64791024952038));
#22745=CARTESIAN_POINT('Ctrl Pts',(12.6441319204139,-0.251254027515963,
4.60062280024232));
#22746=CARTESIAN_POINT('Ctrl Pts',(12.6677460365637,-0.506235857616531,
4.40939182910775));
#22747=CARTESIAN_POINT('Ctrl Pts',(12.6913601527136,-0.639894509617229,
4.12004729681268));
#22748=CARTESIAN_POINT('Ctrl Pts',(12.7149742688635,-0.620198095551099,
3.8019325752266));
#22749=CARTESIAN_POINT('Ctrl Pts',(12.7385883850133,-0.451866840211785,
3.53128609963859));
#22750=CARTESIAN_POINT('Ctrl Pts',(12.7622025011632,-0.17524257447904,3.37297016902465));
#22751=CARTESIAN_POINT('Ctrl Pts',(12.7858166173131,0.143379805101228,3.36492630429559));
#22752=CARTESIAN_POINT('Ctrl Pts',(12.809430733463,0.42764021116234,3.50908227080648));
#22753=CARTESIAN_POINT('Ctrl Pts',(12.8330448496128,0.609413666055986,3.77089008898231));
#22754=CARTESIAN_POINT('Ctrl Pts',(12.8566589657627,0.645136892431096,4.08760569204938));
#22755=CARTESIAN_POINT('Ctrl Pts',(12.8802730819125,0.526248572038732,4.38332598125533));
#22756=CARTESIAN_POINT('Ctrl Pts',(12.9038871980624,0.281241117720374,4.58717953054897));
#22757=CARTESIAN_POINT('Ctrl Pts',(12.9275013142123,-0.0311677281609838,
4.65031141781114));
#22758=CARTESIAN_POINT('Ctrl Pts',(12.9511154303622,-0.336107011072318,
4.55759164674784));
#22759=CARTESIAN_POINT('Ctrl Pts',(12.974729546512,-0.56049590900091,4.33124115596169));
#22760=CARTESIAN_POINT('Ctrl Pts',(12.9983436626619,-0.650558060547343,
4.02550641626558));
#22761=CARTESIAN_POINT('Ctrl Pts',(13.0219577788117,-0.584709444123524,
3.71365888635357));
#22762=CARTESIAN_POINT('Ctrl Pts',(13.0455718949616,-0.378731139057797,
3.47043499764384));
#22763=CARTESIAN_POINT('Ctrl Pts',(13.0691860111115,-0.0819872800401352,
3.35412504823007));
#22764=CARTESIAN_POINT('Ctrl Pts',(13.0928001272613,0.234405401379786,3.39260352716186));
#22765=CARTESIAN_POINT('Ctrl Pts',(13.1164142434112,0.494621196584012,3.57664879910166));
#22766=CARTESIAN_POINT('Ctrl Pts',(13.1400283595611,0.636297578801308,3.86215313342763));
#22767=CARTESIAN_POINT('Ctrl Pts',(13.1636424757109,0.625480816776257,4.18069342892634));
#22768=CARTESIAN_POINT('Ctrl Pts',(13.1872565918608,0.464763222827219,4.45592928631477));
#22769=CARTESIAN_POINT('Ctrl Pts',(13.2108707080107,0.192661887153653,4.62189851635989));
#22770=CARTESIAN_POINT('Ctrl Pts',(13.2344848241605,-0.125612210960856,
4.63882543771344));
#22771=CARTESIAN_POINT('Ctrl Pts',(13.2580989403104,-0.413782468289504,
4.50265339583901));
#22772=CARTESIAN_POINT('Ctrl Pts',(13.2817130564603,-0.602786876612853,
4.24601696851145));
#22773=CARTESIAN_POINT('Ctrl Pts',(13.3053271726101,-0.647329213752593,
3.9304208620728));
#22774=CARTESIAN_POINT('Ctrl Pts',(13.32894128876,-0.536734598538914,3.6314998804023));
#22775=CARTESIAN_POINT('Ctrl Pts',(13.3525554049099,-0.297507800394296,
3.42089251764738));
#22776=CARTESIAN_POINT('Ctrl Pts',(13.3761695210598,0.0130188131672444,
3.34907229440132));
#22777=CARTESIAN_POINT('Ctrl Pts',(13.3997836372096,0.320425377524893,3.43325142712992));
#22778=CARTESIAN_POINT('Ctrl Pts',(13.4233977533595,0.551039769569266,3.65325580067535));
#22779=CARTESIAN_POINT('Ctrl Pts',(13.4470118695093,0.649593644862141,3.95635983539258));
#22780=CARTESIAN_POINT('Ctrl Pts',(13.4706259856592,0.592467881122722,4.26992253935193));
#22781=CARTESIAN_POINT('Ctrl Pts',(13.4942401018091,0.393353065302923,4.5187964277335));
#22782=CARTESIAN_POINT('Ctrl Pts',(13.5178542179589,0.0999684491195412,
4.64333714069132));
#22783=CARTESIAN_POINT('Ctrl Pts',(13.5414683341088,-0.217374301809525,
4.61369762939502));
#22784=CARTESIAN_POINT('Ctrl Pts',(13.5650824502587,-0.482621788093898,
4.43698120905743));
#22785=CARTESIAN_POINT('Ctrl Pts',(13.5886965664085,-0.632205603168059,
4.15553919999523));
#22786=CARTESIAN_POINT('Ctrl Pts',(13.6123106825584,-0.630276944445953,
3.83682113889318));
#22787=CARTESIAN_POINT('Ctrl Pts',(13.6359247987083,-0.477298028416376,
3.55721002779864));
#22788=CARTESIAN_POINT('Ctrl Pts',(13.6595389148582,-0.209931317243796,
3.38371661595291));
#22789=CARTESIAN_POINT('Ctrl Pts',(13.683153031008,0.107746895509167,3.35791980725116));
#22790=CARTESIAN_POINT('Ctrl Pts',(13.7067671471579,0.399602814690774,3.48600198647908));
#22791=CARTESIAN_POINT('Ctrl Pts',(13.7303812633077,0.59569113756138,3.73726736776131));
#22792=CARTESIAN_POINT('Ctrl Pts',(13.7539953794576,0.649017932507905,4.05149845333026));
#22793=CARTESIAN_POINT('Ctrl Pts',(13.7776094956075,0.546803061895555,4.35338757606046));
#22794=CARTESIAN_POINT('Ctrl Pts',(13.8012236117573,0.313543031018869,4.57058490613733));
#22795=CARTESIAN_POINT('Ctrl Pts',(13.8248377279072,0.00514023007941788,
4.65103759142385));
#22796=CARTESIAN_POINT('Ctrl Pts',(13.8484518440571,-0.304494462781446,
4.57546458583277));
#22797=CARTESIAN_POINT('Ctrl Pts',(13.8720659602069,-0.541154937947787,
4.36197748624323));
#22798=CARTESIAN_POINT('Ctrl Pts',(13.8956800763568,-0.648123865072376,
4.06173996222779));
#22799=CARTESIAN_POINT('Ctrl Pts',(13.9192941925067,-0.599765396122921,
3.74670602647169));
#22800=CARTESIAN_POINT('Ctrl Pts',(13.9429083086565,-0.407668974822819,
3.49237575473668));
#22801=CARTESIAN_POINT('Ctrl Pts',(13.9665224248064,-0.117871845784803,
3.35970116712309));
#22802=CARTESIAN_POINT('Ctrl Pts',(13.9901365409563,0.200174091641329,3.38047865214521));
#22803=CARTESIAN_POINT('Ctrl Pts',(14.0137506571061,0.470246914526057,3.54972874087838));
#22804=CARTESIAN_POINT('Ctrl Pts',(14.037364773256,0.627621790796785,3.82688947135059));
#22805=CARTESIAN_POINT('Ctrl Pts',(14.0609788894059,0.634582735815489,4.14553734509456));
#22806=CARTESIAN_POINT('Ctrl Pts',(14.0845930055557,0.489461510650943,4.42930618095194));
#22807=CARTESIAN_POINT('Ctrl Pts',(14.1082071217056,0.227037427151766,4.61018880199865));
#22808=CARTESIAN_POINT('Ctrl Pts',(14.1318212378555,-0.0897977562486571,
4.64483542891575));
#22809=CARTESIAN_POINT('Ctrl Pts',(14.1554353540053,-0.385112282251534,
4.52494275637564));
#22810=CARTESIAN_POINT('Ctrl Pts',(14.1790494701552,-0.588131968915973,
4.27924389796604));
#22811=CARTESIAN_POINT('Ctrl Pts',(14.2026635863051,-0.65020173504413,3.96662229549764));
#22812=CARTESIAN_POINT('Ctrl Pts',(14.2262777024549,-0.556446129094758,
3.66199989226673));
#22813=CARTESIAN_POINT('Ctrl Pts',(14.2498918186048,-0.329334334698108,
3.43838156778717));
#22814=CARTESIAN_POINT('Ctrl Pts',(14.2735059347547,-0.0232952743833569,
3.34935901020328));
#22815=CARTESIAN_POINT('Ctrl Pts',(14.2971200509045,0.28832666060365,3.41626709515619));
#22816=CARTESIAN_POINT('Ctrl Pts',(14.3207341670544,0.530849104237583,3.62307083431711));
#22817=CARTESIAN_POINT('Ctrl Pts',(14.3443482832043,0.646149864620809,3.92020827196535));
#22818=CARTESIAN_POINT('Ctrl Pts',(14.3679623993541,0.606596311879891,4.2364683526943));
#22819=CARTESIAN_POINT('Ctrl Pts',(14.391576515504,0.42166773027486,4.49605714656388));
#22820=CARTESIAN_POINT('Ctrl Pts',(14.4151906316539,0.135683541737747,4.63676239203782));
#22821=CARTESIAN_POINT('Ctrl Pts',(14.4388047478037,-0.182818152115814,
4.62486309754155));
#22822=CARTESIAN_POINT('Ctrl Pts',(14.4624188639536,-0.457506203155893,
4.46321101183598));
#22823=CARTESIAN_POINT('Ctrl Pts',(14.4860329801035,-0.622549707754089,
4.19054718257559));
#22824=CARTESIAN_POINT('Ctrl Pts',(14.5096470962533,-0.63839484111024,3.87221739454711));
#22825=CARTESIAN_POINT('Ctrl Pts',(14.5332612124032,-0.501244206711231,
3.58451159745434));
#22826=CARTESIAN_POINT('Ctrl Pts',(14.5568753285531,-0.243966908844842,
3.39638048838484));
#22827=CARTESIAN_POINT('Ctrl Pts',(14.5804894447029,0.0717787570654544,
3.35291099727801));
#22828=CARTESIAN_POINT('Ctrl Pts',(14.6041035608528,0.370322144162233,3.46452089026927));
#22829=CARTESIAN_POINT('Ctrl Pts',(14.6277176770027,0.580115251486915,3.70446207957941));
#22830=CARTESIAN_POINT('Ctrl Pts',(14.6513317931525,0.650879700384091,4.0152309888134));
#22831=CARTESIAN_POINT('Ctrl Pts',(14.6749459093024,0.565656298155129,4.32234968564526));
#22832=CARTESIAN_POINT('Ctrl Pts',(14.6985600254523,0.344869426209941,4.55221503612336));
#22833=CARTESIAN_POINT('Ctrl Pts',(14.7221741416021,0.041432195817608,4.64973820947522));
#22834=CARTESIAN_POINT('Ctrl Pts',(14.745788257752,-0.271934549361806,4.59154709694401));
#22835=CARTESIAN_POINT('Ctrl Pts',(14.7694023739019,-0.520130285395982,
4.39158760667368));
#22836=CARTESIAN_POINT('Ctrl Pts',(14.7930164900517,-0.64367318065081,4.09778141619902));
#22837=CARTESIAN_POINT('Ctrl Pts',(14.8166306062016,-0.612955311082805,
3.78054123783642));
#22838=CARTESIAN_POINT('Ctrl Pts',(14.8402447223515,-0.435338447621071,
3.51589585985611));
#22839=CARTESIAN_POINT('Ctrl Pts',(14.8638588385013,-0.153389665944836,
3.36726945127358));
#22840=CARTESIAN_POINT('Ctrl Pts',(14.8874729546512,0.165319955489652,3.37028123293502));
#22841=CARTESIAN_POINT('Ctrl Pts',(14.9110870708011,0.444409630539555,3.52420969451069));
#22842=CARTESIAN_POINT('Ctrl Pts',(14.9347011869509,0.616993161964042,3.79216419995926));
#22843=CARTESIAN_POINT('Ctrl Pts',(14.9583153031008,0.641710593195818,4.10992889087348));
#22844=CARTESIAN_POINT('Ctrl Pts',(14.9819294192507,0.512636325700993,4.40134645341462));
#22845=CARTESIAN_POINT('Ctrl Pts',(15.0055435354005,0.260708010403211,4.59658262768273));
#22846=CARTESIAN_POINT('Ctrl Pts',(15.0291576515504,-0.0537065278721878,
4.64883488988255));
#22847=CARTESIAN_POINT('Ctrl Pts',(15.0527717677003,-0.355236031271534,
4.54560815721762));
#22848=CARTESIAN_POINT('Ctrl Pts',(15.0763858838501,-0.571652475026301,
4.31158258982903));
#22849=CARTESIAN_POINT('Ctrl Pts',(15.09212862795,-0.624530364890795,4.10584538053252));
#22850=CARTESIAN_POINT('Ctrl Pts',(15.1,-0.624993681275899,4.00281040303152));
#22851=CARTESIAN_POINT('Ctrl Pts',(15.1,-0.624993681275899,4.00281040303152));
#22852=CARTESIAN_POINT('Ctrl Pts',(15.1,-0.617358358083874,4.02914127082806));
#22853=CARTESIAN_POINT('Ctrl Pts',(15.1,-0.607931963506944,4.05484759228836));
#22854=CARTESIAN_POINT('Ctrl Pts',(15.1,-0.596773861259576,4.07974656001827));
#22855=CARTESIAN_POINT('Ctrl Pts',(15.1,-0.585871522029423,4.10407480030985));
#22856=CARTESIAN_POINT('Ctrl Pts',(15.1,-0.573314772633929,4.12763281365198));
#22857=CARTESIAN_POINT('Ctrl Pts',(15.1,-0.559143639302279,4.1502040881484));
#22858=CARTESIAN_POINT('Ctrl Pts',(15.1,-0.549626121151564,4.16536325076984));
#22859=CARTESIAN_POINT('Ctrl Pts',(15.1,-0.539380106047495,4.18007635520315));
#22860=CARTESIAN_POINT('Ctrl Pts',(15.1,-0.528417753985571,4.19426420824267));
#22861=CARTESIAN_POINT('Ctrl Pts',(15.1,-0.523814643226911,4.2002217124899));
#22862=CARTESIAN_POINT('Ctrl Pts',(15.1,-0.519084627089791,4.20608691507751));
#22863=CARTESIAN_POINT('Ctrl Pts',(15.1,-0.514239086396905,4.21184190560023));
#22864=CARTESIAN_POINT('Ctrl Pts',(15.1,-0.50085552272952,4.2277374035328));
#22865=CARTESIAN_POINT('Ctrl Pts',(15.1,-0.486572803760524,4.24281789068328));
#22866=CARTESIAN_POINT('Ctrl Pts',(15.1,-0.4714177983537,4.25697008589974));
#22867=CARTESIAN_POINT('Ctrl Pts',(15.1,-0.457151696655403,4.27029219637033));
#22868=CARTESIAN_POINT('Ctrl Pts',(15.1,-0.442112042545397,4.28279146400573));
#22869=CARTESIAN_POINT('Ctrl Pts',(15.1,-0.426369607892924,4.29437520287289));
#22870=CARTESIAN_POINT('Ctrl Pts',(15.1,-0.419074661497203,4.29974303548351));
#22871=CARTESIAN_POINT('Ctrl Pts',(15.1,-0.411628924918527,4.30491398987477));
#22872=CARTESIAN_POINT('Ctrl Pts',(15.1,-0.404040271526401,4.30987739070861));
#22873=CARTESIAN_POINT('Ctrl Pts',(15.1,-0.398073367501634,4.31378007737535));
#22874=CARTESIAN_POINT('Ctrl Pts',(15.1,-0.392026704362881,4.31754881952869));
#22875=CARTESIAN_POINT('Ctrl Pts',(15.1,-0.385904261325812,4.32117966642505));
#22876=CARTESIAN_POINT('Ctrl Pts',(15.1,-0.366868686798561,4.33246850264191));
#22877=CARTESIAN_POINT('Ctrl Pts',(15.1,-0.347097727375919,4.34242824684389));
#22878=CARTESIAN_POINT('Ctrl Pts',(15.1,-0.326713262272485,4.3509180109496));
#22879=CARTESIAN_POINT('Ctrl Pts',(15.1,-0.308010762698638,4.35870726657947));
#22880=CARTESIAN_POINT('Ctrl Pts',(15.1,-0.288791261952878,4.36525839133365));
#22881=CARTESIAN_POINT('Ctrl Pts',(15.1,-0.269173508333929,4.37043259773196));
#22882=CARTESIAN_POINT('Ctrl Pts',(12.5,-0.186196943290592,3.58169363627332));
#22883=CARTESIAN_POINT('Ctrl Pts',(12.5,-0.170588484282379,3.56594316788148));
#22884=CARTESIAN_POINT('Ctrl Pts',(12.5,-0.153797667832464,3.55144458439849));
#22885=CARTESIAN_POINT('Ctrl Pts',(12.5,-0.136060690067392,3.53823162417247));
#22886=CARTESIAN_POINT('Ctrl Pts',(12.5,-0.117990710310259,3.5247705978929));
#22887=CARTESIAN_POINT('Ctrl Pts',(12.5,-0.0989385549429972,3.51264262455394));
#22888=CARTESIAN_POINT('Ctrl Pts',(12.5,-0.0790990435859813,3.5018744512649));
#22889=CARTESIAN_POINT('Ctrl Pts',(12.5,-0.0668145727052721,3.49520688224936));
#22890=CARTESIAN_POINT('Ctrl Pts',(12.5,-0.054227138249592,3.4890605701039));
#22891=CARTESIAN_POINT('Ctrl Pts',(12.5,-0.0413735013057162,3.4834433907237));
#22892=CARTESIAN_POINT('Ctrl Pts',(12.5,-0.0353493612034326,3.48081077586818));
#22893=CARTESIAN_POINT('Ctrl Pts',(12.5,-0.0292710672153644,3.47829647656688));
#22894=CARTESIAN_POINT('Ctrl Pts',(12.5,-0.0231507758853709,3.47590397706369));
#22895=CARTESIAN_POINT('Ctrl Pts',(12.5,-0.00211397253512804,3.467680423829));
#22896=CARTESIAN_POINT('Ctrl Pts',(12.5,0.0194422610390746,3.46088402724794));
#22897=CARTESIAN_POINT('Ctrl Pts',(12.5,0.0413436963816045,3.45552737346533));
#22898=CARTESIAN_POINT('Ctrl Pts',(12.5,0.0650920698750741,3.44971899548849));
#22899=CARTESIAN_POINT('Ctrl Pts',(12.5,0.089246474293393,3.44560199012534));
#22900=CARTESIAN_POINT('Ctrl Pts',(12.5,0.113633446029948,3.44311473184586));
#22901=CARTESIAN_POINT('Ctrl Pts',(12.5,0.123118497624279,3.44214733936417));
#22902=CARTESIAN_POINT('Ctrl Pts',(12.5,0.132642564327611,3.44142688205345));
#22903=CARTESIAN_POINT('Ctrl Pts',(12.5,0.142169452875131,3.44095138714122));
#22904=CARTESIAN_POINT('Ctrl Pts',(12.5,0.170359862108328,3.43954438042575));
#22905=CARTESIAN_POINT('Ctrl Pts',(12.5,0.19861482332424,3.44027367679077));
#22906=CARTESIAN_POINT('Ctrl Pts',(12.5,0.226679319731597,3.44302987267532));
#22907=CARTESIAN_POINT('Ctrl Pts',(12.5,0.254743816138955,3.44578606855986));
#22908=CARTESIAN_POINT('Ctrl Pts',(12.5,0.282619254593541,3.45056842907764));
#22909=CARTESIAN_POINT('Ctrl Pts',(12.5,0.310093463203745,3.45730861053194));
#22910=CARTESIAN_POINT('Ctrl Pts',(15.0699957084852,-1.05870731373636E-5,
4.45788944868556));
#22911=CARTESIAN_POINT('Ctrl Pts',(15.0634386537186,0.0628625045491076,
4.45782850550181));
#22912=CARTESIAN_POINT('Ctrl Pts',(15.0568815989521,0.125761012144406,4.44477074790967));
#22913=CARTESIAN_POINT('Ctrl Pts',(15.0503245441856,0.183365120595825,4.41959809737683));
#22914=CARTESIAN_POINT('Ctrl Pts',(15.0424531721356,0.252515583017112,4.38937975928409));
#22915=CARTESIAN_POINT('Ctrl Pts',(15.0345818000857,0.314036477612831,4.34170308552782));
#22916=CARTESIAN_POINT('Ctrl Pts',(15.0267104280357,0.360556892971808,4.28228266426341));
#22917=CARTESIAN_POINT('Ctrl Pts',(15.0188390559858,0.407077308330786,4.222862242999));
#22918=CARTESIAN_POINT('Ctrl Pts',(15.0109676839358,0.438597244453022,4.15169807422645));
#22919=CARTESIAN_POINT('Ctrl Pts',(15.0030963118859,0.45133921416074,4.07731692107955));
#22920=CARTESIAN_POINT('Ctrl Pts',(14.9952249398359,0.464081183868457,4.00293576793266));
#22921=CARTESIAN_POINT('Ctrl Pts',(14.9873535677859,0.458045187161657,3.92533763041141));
#22922=CARTESIAN_POINT('Ctrl Pts',(14.979482195736,0.433954739621328,3.85382131653551));
#22923=CARTESIAN_POINT('Ctrl Pts',(14.971610823686,0.409864292080999,3.78230500265962));
#22924=CARTESIAN_POINT('Ctrl Pts',(14.9637394516361,0.367719393707138,3.71687051242907));
#22925=CARTESIAN_POINT('Ctrl Pts',(14.9558680795861,0.312570095196614,3.66535860215541));
#22926=CARTESIAN_POINT('Ctrl Pts',(14.9479967075362,0.257420796686091,3.61384669188175));
#22927=CARTESIAN_POINT('Ctrl Pts',(14.9401253354862,0.189267098038905,3.57625736156498));
#22928=CARTESIAN_POINT('Ctrl Pts',(14.9322539634362,0.116275803938161,3.55709495786573));
#22929=CARTESIAN_POINT('Ctrl Pts',(14.9243825913863,0.0432845098374172,
3.53793255416647));
#22930=CARTESIAN_POINT('Ctrl Pts',(14.9165112193363,-0.0345443797168851,
3.53719707708475));
#22931=CARTESIAN_POINT('Ctrl Pts',(14.9086398472864,-0.107884770736704,
3.55497662303181));
#22932=CARTESIAN_POINT('Ctrl Pts',(14.9007684752364,-0.181225161756525,
3.57275616897888));
#22933=CARTESIAN_POINT('Ctrl Pts',(14.8928971031865,-0.250077054241862,
3.60905073795473));
#22934=CARTESIAN_POINT('Ctrl Pts',(14.8850257311365,-0.306190019513209,
3.65951122309406));
#22935=CARTESIAN_POINT('Ctrl Pts',(14.8771543590866,-0.362302984784554,
3.70997170823338));
#22936=CARTESIAN_POINT('Ctrl Pts',(14.8692829870366,-0.405677022841909,
3.77459810953617));
#22937=CARTESIAN_POINT('Ctrl Pts',(14.8614116149867,-0.431114693744839,
3.84564633596564));
#22938=CARTESIAN_POINT('Ctrl Pts',(14.8535402429367,-0.45655236464777,3.91669456239511));
#22939=CARTESIAN_POINT('Ctrl Pts',(14.8456688708867,-0.464053668396277,
3.99416461395126));
#22940=CARTESIAN_POINT('Ctrl Pts',(14.8377974988368,-0.452719732759917,
4.06877337558629));
#22941=CARTESIAN_POINT('Ctrl Pts',(14.8299261267868,-0.441385797123556,
4.14338213722132));
#22942=CARTESIAN_POINT('Ctrl Pts',(14.8220547547369,-0.411216622102327,
4.21512960893523));
#22943=CARTESIAN_POINT('Ctrl Pts',(14.8141833826869,-0.365827335221939,
4.27541839855419));
#22944=CARTESIAN_POINT('Ctrl Pts',(14.806312010637,-0.32043804834155,4.33570718817315));
#22945=CARTESIAN_POINT('Ctrl Pts',(14.798440638587,-0.259828649602004,4.38453729569717));
#22946=CARTESIAN_POINT('Ctrl Pts',(14.7905692665371,-0.191261870645823,
4.41605748429924));
#22947=CARTESIAN_POINT('Ctrl Pts',(14.7837114138531,-0.131523763221734,
4.44351912740692));
#22948=CARTESIAN_POINT('Ctrl Pts',(14.7768535611691,-0.065745536276614,
4.45784152413683));
#22949=CARTESIAN_POINT('Ctrl Pts',(14.7699957084852,8.6346448269735E-6,
4.45789857801605));
#22950=CARTESIAN_POINT('Ctrl Pts',(12.5,0.310062960217722,4.54266560670548));
#22951=CARTESIAN_POINT('Ctrl Pts',(12.50787137205,0.220600394030941,4.59378185169648));
#22952=CARTESIAN_POINT('Ctrl Pts',(12.5236141161499,0.0159878432799406,
4.65085692712531));
#22953=CARTESIAN_POINT('Ctrl Pts',(12.5472282322997,-0.294892507759568,
4.580447501361));
#22954=CARTESIAN_POINT('Ctrl Pts',(12.5708423484496,-0.535054221536356,
4.37092866956447));
#22955=CARTESIAN_POINT('Ctrl Pts',(12.5944564645995,-0.647009713430093,
4.07251155115386));
#22956=CARTESIAN_POINT('Ctrl Pts',(12.6180705807493,-0.603894380709874,
3.75671714932517));
#22957=CARTESIAN_POINT('Ctrl Pts',(12.6416846968992,-0.416056506175611,
3.49922677321964));
#22958=CARTESIAN_POINT('Ctrl Pts',(12.6652988130491,-0.128505496873939,
3.36175035317655));
#22959=CARTESIAN_POINT('Ctrl Pts',(12.6889129291989,0.189841674427298,3.37723482234205));
#22960=CARTESIAN_POINT('Ctrl Pts',(12.7125270453488,0.462692468193658,3.54196933898577));
#22961=CARTESIAN_POINT('Ctrl Pts',(12.7361411614987,0.624655556881011,3.81647407445394));
#22962=CARTESIAN_POINT('Ctrl Pts',(12.7597552776485,0.636915702199809,4.13496208375113));
#22963=CARTESIAN_POINT('Ctrl Pts',(12.7833693937984,0.496534514683115,4.42110548633398));
#22964=CARTESIAN_POINT('Ctrl Pts',(12.8069835099483,0.237155397994168,4.60632802944461));
#22965=CARTESIAN_POINT('Ctrl Pts',(12.8305976260981,-0.0790596718614395,
4.64623983861064));
#22966=CARTESIAN_POINT('Ctrl Pts',(12.854211742248,-0.376327535803878,4.5312757721487));
#22967=CARTESIAN_POINT('Ctrl Pts',(12.8778258583979,-0.583405888470749,
4.28898776831928));
#22968=CARTESIAN_POINT('Ctrl Pts',(12.9014399745477,-0.650666957548692,
3.97744183415536));
#22969=CARTESIAN_POINT('Ctrl Pts',(12.9250540906976,-0.561991161265395,
3.67130212143154));
#22970=CARTESIAN_POINT('Ctrl Pts',(12.9486682068475,-0.338630270727757,
3.44393714350224));
#22971=CARTESIAN_POINT('Ctrl Pts',(12.9722823229973,-0.0341142786054444,
3.34983650006563));
#22972=CARTESIAN_POINT('Ctrl Pts',(12.9958964391472,0.278577437919422,3.41155206540036));
#22973=CARTESIAN_POINT('Ctrl Pts',(13.0195105552971,0.524506132150044,3.61429327464512));
#22974=CARTESIAN_POINT('Ctrl Pts',(13.0431246714469,0.644733280558021,3.90947178565704));
#22975=CARTESIAN_POINT('Ctrl Pts',(13.0667387875968,0.61044561006836,4.22634601343335));
#22976=CARTESIAN_POINT('Ctrl Pts',(13.0903529037467,0.429860399609997,4.4889748434194));
#22977=CARTESIAN_POINT('Ctrl Pts',(13.1139670198965,0.146256151980267,4.63441744826062));
#22978=CARTESIAN_POINT('Ctrl Pts',(13.1375811360464,-0.172399400609521,
4.62781749523177));
#22979=CARTESIAN_POINT('Ctrl Pts',(13.1611952521963,-0.449738236712957,
4.47075670902068));
#22980=CARTESIAN_POINT('Ctrl Pts',(13.1848093683461,-0.619294173608025,
4.2008758003961));
#22981=CARTESIAN_POINT('Ctrl Pts',(13.208423484496,-0.64043195068177,3.88285360784221));
#22982=CARTESIAN_POINT('Ctrl Pts',(13.2320376006459,-0.508085752511173,
3.59290636366459));
#22983=CARTESIAN_POINT('Ctrl Pts',(13.2556517167957,-0.253973266794505,
3.40052194335125));
#22984=CARTESIAN_POINT('Ctrl Pts',(13.2792658329456,0.0610056803032868,
3.3518066124833));
#22985=CARTESIAN_POINT('Ctrl Pts',(13.3028799490955,0.361364191435218,3.45843533922715));
#22986=CARTESIAN_POINT('Ctrl Pts',(13.3264940652453,0.575119258511334,3.69485380694));
#22987=CARTESIAN_POINT('Ctrl Pts',(13.3501081813952,0.65104299168552,4.00440268404554));
#22988=CARTESIAN_POINT('Ctrl Pts',(13.3737222975451,0.570939739771795,4.31289642727099));
#22989=CARTESIAN_POINT('Ctrl Pts',(13.3973364136949,0.354006804717113,4.54640236352309));
#22990=CARTESIAN_POINT('Ctrl Pts',(13.4209505298448,0.0522336745508671,
4.6489591696652));
#22991=CARTESIAN_POINT('Ctrl Pts',(13.4445646459947,-0.26205761933777,4.59598839317277));
#22992=CARTESIAN_POINT('Ctrl Pts',(13.4681787621445,-0.513544980480383,
4.40018484937968));
#22993=CARTESIAN_POINT('Ctrl Pts',(13.4917928782944,-0.64195771209056,4.10847422061066));
#22994=CARTESIAN_POINT('Ctrl Pts',(13.5154069944443,-0.616520809113462,
3.79076698974655));
#22995=CARTESIAN_POINT('Ctrl Pts',(13.5390211105941,-0.443330402422436,
3.52320390633144));
#22996=CARTESIAN_POINT('Ctrl Pts',(13.562635226744,-0.163892778617988,3.36990832590288));
#22997=CARTESIAN_POINT('Ctrl Pts',(13.5862493428939,0.154822890495328,3.36761860145296));
#22998=CARTESIAN_POINT('Ctrl Pts',(13.6098634590437,0.43643417612693,3.51688348138565));
#22999=CARTESIAN_POINT('Ctrl Pts',(13.6334775751936,0.613450973283793,3.78193059814177));
#23000=CARTESIAN_POINT('Ctrl Pts',(13.6570916913435,0.643449974253473,4.09923956510808));
#23001=CARTESIAN_POINT('Ctrl Pts',(13.6807058074933,0.519241709620395,4.39276507945606));
#23002=CARTESIAN_POINT('Ctrl Pts',(13.7043199236432,0.270593554659618,4.59216170834183));
#23003=CARTESIAN_POINT('Ctrl Pts',(13.7279340397931,-0.0429042293685969,
4.64964266158552));
#23004=CARTESIAN_POINT('Ctrl Pts',(13.7515481559429,-0.346119716157775,
4.55143222859795));
#23005=CARTESIAN_POINT('Ctrl Pts',(13.7751622720928,-0.566385203513325,
4.32106722332061));
#23006=CARTESIAN_POINT('Ctrl Pts',(13.7987763882427,-0.650912534047929,
4.01375622291695));
#23007=CARTESIAN_POINT('Ctrl Pts',(13.8223905043925,-0.57944414457563,3.70314844792952));
#23008=CARTESIAN_POINT('Ctrl Pts',(13.8460046205424,-0.369107932149097,
3.46368321387984));
#23009=CARTESIAN_POINT('Ctrl Pts',(13.8696187366923,-0.0703124342978696,
3.35275003110641));
#23010=CARTESIAN_POINT('Ctrl Pts',(13.8932328528421,0.245333927901481,3.3969348091043));
#23011=CARTESIAN_POINT('Ctrl Pts',(13.916846968992,0.502184306426786,3.58564835824111));
#23012=CARTESIAN_POINT('Ctrl Pts',(13.9404610851419,0.638682720042094,3.87366416276737));
#23013=CARTESIAN_POINT('Ctrl Pts',(13.9640752012917,0.62211637371287,4.19195723015293));
#23014=CARTESIAN_POINT('Ctrl Pts',(13.9876893174416,0.456455507660852,4.46424641105313));
#23015=CARTESIAN_POINT('Ctrl Pts',(14.0113034335915,0.181401901656729,4.62527570776815));
#23016=CARTESIAN_POINT('Ctrl Pts',(14.0349175497413,-0.137125932879425,
4.63645332836083));
#23017=CARTESIAN_POINT('Ctrl Pts',(14.0585316658912,-0.422790583021024,
4.49510047824495));
#23018=CARTESIAN_POINT('Ctrl Pts',(14.0821457820411,-0.60713052675338,4.23509335195577));
#23019=CARTESIAN_POINT('Ctrl Pts',(14.1057598981909,-0.645967413308333,
3.91874446730605));
#23020=CARTESIAN_POINT('Ctrl Pts',(14.1293740143408,-0.529993712466286,
3.62186903671368));
#23021=CARTESIAN_POINT('Ctrl Pts',(14.1529881304907,-0.287003328966194,
3.41561532377041));
#23022=CARTESIAN_POINT('Ctrl Pts',(14.1766022466405,0.0247694002478971,
3.34941346658496));
#23023=CARTESIAN_POINT('Ctrl Pts',(14.2002163627904,0.330605970264406,3.43912920108534));
#23024=CARTESIAN_POINT('Ctrl Pts',(14.2238304789403,0.557210518047066,3.66326152695696));
#23025=CARTESIAN_POINT('Ctrl Pts',(14.2474445950901,0.650275686248857,3.96809557204375));
#23026=CARTESIAN_POINT('Ctrl Pts',(14.27105871124,0.587497759452106,4.28057573538778));
#23027=CARTESIAN_POINT('Ctrl Pts',(14.2946728273899,0.383921904832036,4.52581397056352));
#23028=CARTESIAN_POINT('Ctrl Pts',(14.3182869435397,0.088336493108731,4.64503722732482));
#23029=CARTESIAN_POINT('Ctrl Pts',(14.3419010596896,-0.22841937412829,4.6096728222354));
#23030=CARTESIAN_POINT('Ctrl Pts',(14.3655151758395,-0.490432948250941,
4.42819608115853));
#23031=CARTESIAN_POINT('Ctrl Pts',(14.3891292919893,-0.634910852255616,
4.14409916841427));
#23032=CARTESIAN_POINT('Ctrl Pts',(14.4127434081392,-0.627227950688033,
3.82546788683648));
#23033=CARTESIAN_POINT('Ctrl Pts',(14.4363575242891,-0.469225504392149,
3.54866444115539));
#23034=CARTESIAN_POINT('Ctrl Pts',(14.4599716404389,-0.198769899531221,
3.38002670405092));
#23035=CARTESIAN_POINT('Ctrl Pts',(14.4835857565888,0.11932229545683,3.35996988316441));
#23036=CARTESIAN_POINT('Ctrl Pts',(14.5071998727387,0.408818071695872,3.49330073524378));
#23037=CARTESIAN_POINT('Ctrl Pts',(14.5308139888885,0.600337751131954,3.74806559342675));
#23038=CARTESIAN_POINT('Ctrl Pts',(14.5544281050384,0.647982309355475,4.06320828594604));
#23039=CARTESIAN_POINT('Ctrl Pts',(14.5780422211883,0.540333396317157,4.36320267272319));
#23040=CARTESIAN_POINT('Ctrl Pts',(14.6016563373381,0.303189823409542,4.57615301060753));
#23041=CARTESIAN_POINT('Ctrl Pts',(14.625270453488,-0.00661530128860875,
4.65102426869959));
#23042=CARTESIAN_POINT('Ctrl Pts',(14.6488845696379,-0.314835022974042,
4.56987302880665));
#23043=CARTESIAN_POINT('Ctrl Pts',(14.6724986857877,-0.547602339746838,
4.35214775046202));
#23044=CARTESIAN_POINT('Ctrl Pts',(14.6961128019376,-0.649132943719538,
4.05002781234082));
#23045=CARTESIAN_POINT('Ctrl Pts',(14.7197269180875,-0.595094318970103,
3.73591836064326));
#23046=CARTESIAN_POINT('Ctrl Pts',(14.7433410342373,-0.398437197867616,
3.48509791236843));
#23047=CARTESIAN_POINT('Ctrl Pts',(14.7669551503872,-0.1062918289807,3.35767733339665));
#23048=CARTESIAN_POINT('Ctrl Pts',(14.7905692665371,0.211327117384507,3.38419385377023));
#23049=CARTESIAN_POINT('Ctrl Pts',(14.8141833826869,0.478300047385911,3.5582926020622));
#23050=CARTESIAN_POINT('Ctrl Pts',(14.8377974988368,0.630645044771057,3.83824960712979));
#23051=CARTESIAN_POINT('Ctrl Pts',(14.8614116149867,0.631851559871185,4.15697121131127));
#23052=CARTESIAN_POINT('Ctrl Pts',(14.8850257311365,0.481630465478622,4.4380735902585));
#23053=CARTESIAN_POINT('Ctrl Pts',(14.9086398472864,0.215983244330552,4.61418854455152));
#23054=CARTESIAN_POINT('Ctrl Pts',(14.9322539634363,-0.101425794369151,
4.64310902247508));
#23055=CARTESIAN_POINT('Ctrl Pts',(14.9558680795861,-0.394527586443172,
4.517903766532));
#23056=CARTESIAN_POINT('Ctrl Pts',(14.979482195736,-0.593077772790822,4.26857965265179));
#23057=CARTESIAN_POINT('Ctrl Pts',(15.0030963118859,-0.649493436571599,
3.95488773069898));
#23058=CARTESIAN_POINT('Ctrl Pts',(15.0267104280357,-0.550252000240565,
3.65200904506483));
#23059=CARTESIAN_POINT('Ctrl Pts',(15.0503245441856,-0.319142060764588,
3.43252503194012));
#23060=CARTESIAN_POINT('Ctrl Pts',(15.0739386603355,-0.0115409051696555,
3.34904846156061));
#23061=CARTESIAN_POINT('Ctrl Pts',(15.0975527764853,0.298810377697559,3.42155963907315));
#23062=CARTESIAN_POINT('Ctrl Pts',(15.1211668926352,0.537575400322941,3.63273573589665));
#23063=CARTESIAN_POINT('Ctrl Pts',(15.1369096367351,0.610790903144771,3.83214323401692));
#23064=CARTESIAN_POINT('Ctrl Pts',(15.1447810087851,0.621570310124627,3.93461384266089));
#23065=CARTESIAN_POINT('Ctrl Pts',(12.4850729970716,0.282426015030316,4.49429601229446));
#23066=CARTESIAN_POINT('Ctrl Pts',(12.4929443691216,0.200937545576316,4.54085609598193));
#23067=CARTESIAN_POINT('Ctrl Pts',(12.5086871132215,0.0145627935155885,
4.59284387968754));
#23068=CARTESIAN_POINT('Ctrl Pts',(12.5323012293714,-0.268607755567932,
4.52871028073968));
#23069=CARTESIAN_POINT('Ctrl Pts',(12.5559153455213,-0.487363055256749,
4.3378665608173));
#23070=CARTESIAN_POINT('Ctrl Pts',(12.5795294616711,-0.589339580973024,
4.06604835489435));
#23071=CARTESIAN_POINT('Ctrl Pts',(12.603143577821,-0.550067261575934,3.77840176074865));
#23072=CARTESIAN_POINT('Ctrl Pts',(12.6267576939709,-0.378972002925158,
3.54386236016666));
#23073=CARTESIAN_POINT('Ctrl Pts',(12.6503718101207,-0.117051373585908,
3.41863967169675));
#23074=CARTESIAN_POINT('Ctrl Pts',(12.6739859262706,0.172920453180012,3.43274395851062));
#23075=CARTESIAN_POINT('Ctrl Pts',(12.6976000424204,0.42145114619533,3.58279513857084));
#23076=CARTESIAN_POINT('Ctrl Pts',(12.7212141585703,0.568977924911017,3.83283235195095));
#23077=CARTESIAN_POINT('Ctrl Pts',(12.7448282747202,0.580145282610399,4.12293246335278));
#23078=CARTESIAN_POINT('Ctrl Pts',(12.76844239087,0.45227673827436,4.38357095065208));
#23079=CARTESIAN_POINT('Ctrl Pts',(12.7920565070199,0.216016946852954,4.55228399108678));
#23080=CARTESIAN_POINT('Ctrl Pts',(12.8156706231698,-0.0720128197761896,
4.58863832766248));
#23081=CARTESIAN_POINT('Ctrl Pts',(12.8392847393196,-0.34278420811256,4.48392139165784));
#23082=CARTESIAN_POINT('Ctrl Pts',(12.8628988554695,-0.531404976945056,
4.26322932523642));
#23083=CARTESIAN_POINT('Ctrl Pts',(12.8865129716194,-0.592670842732518,
3.97945251867098));
#23084=CARTESIAN_POINT('Ctrl Pts',(12.9101270877692,-0.51189901575794,3.70060005900794));
#23085=CARTESIAN_POINT('Ctrl Pts',(12.9337412039191,-0.308447025930223,
3.49350087944474));
#23086=CARTESIAN_POINT('Ctrl Pts',(12.957355320069,-0.0310735592390789,
3.40778774002645));
#23087=CARTESIAN_POINT('Ctrl Pts',(12.9809694362188,0.253746902286204,3.46400239130434));
#23088=CARTESIAN_POINT('Ctrl Pts',(13.0045835523687,0.477755152237737,3.64867260076509));
#23089=CARTESIAN_POINT('Ctrl Pts',(13.0281976685186,0.587266054150949,3.91754086716214));
#23090=CARTESIAN_POINT('Ctrl Pts',(13.0518117846685,0.556034558024266,4.20617103876933));
#23091=CARTESIAN_POINT('Ctrl Pts',(13.0754259008183,0.391545509324759,4.44539088570928));
#23092=CARTESIAN_POINT('Ctrl Pts',(13.0990400169682,0.133219853633759,4.57786970637232));
#23093=CARTESIAN_POINT('Ctrl Pts',(13.122654133118,-0.157032867368526,4.57185802915678));
#23094=CARTESIAN_POINT('Ctrl Pts',(13.1462682492679,-0.409651568547275,
4.42879659435664));
#23095=CARTESIAN_POINT('Ctrl Pts',(13.1698823654178,-0.564094419600429,
4.1829710707208));
#23096=CARTESIAN_POINT('Ctrl Pts',(13.1934964815676,-0.583348116144335,
3.89329525626321));
#23097=CARTESIAN_POINT('Ctrl Pts',(13.2171105977175,-0.462798375770677,
3.62919197644995));
#23098=CARTESIAN_POINT('Ctrl Pts',(13.2407247138674,-0.231335782947555,
3.45395542080054));
#23099=CARTESIAN_POINT('Ctrl Pts',(13.2643388300172,0.055568040665587,3.40958224975729));
#23100=CARTESIAN_POINT('Ctrl Pts',(13.2879529461671,0.329154596505292,3.50670680265737));
#23101=CARTESIAN_POINT('Ctrl Pts',(13.311567062317,0.523856961936024,3.72205250428141));
#23102=CARTESIAN_POINT('Ctrl Pts',(13.3351811784668,0.593013359693284,4.00401025814095));
#23103=CARTESIAN_POINT('Ctrl Pts',(13.3587952946167,0.520049977633468,4.28500692572024));
#23104=CARTESIAN_POINT('Ctrl Pts',(13.3824094107666,0.322452998189994,4.49769969952106));
#23105=CARTESIAN_POINT('Ctrl Pts',(13.4060235269164,0.0475779130258999,
4.59111527567571));
#23106=CARTESIAN_POINT('Ctrl Pts',(13.4296376430663,-0.238699550200797,
4.5428659610613));
#23107=CARTESIAN_POINT('Ctrl Pts',(13.4532517592162,-0.467771004553565,
4.36451503980497));
#23108=CARTESIAN_POINT('Ctrl Pts',(13.476865875366,-0.584737881352888,4.09880555174689));
#23109=CARTESIAN_POINT('Ctrl Pts',(13.5004799915159,-0.561568254327815,
3.80941662539381));
#23110=CARTESIAN_POINT('Ctrl Pts',(13.5240941076658,-0.403814885886516,
3.56570233148043));
#23111=CARTESIAN_POINT('Ctrl Pts',(13.5477082238157,-0.149284468950505,
3.42607049712074));
#23112=CARTESIAN_POINT('Ctrl Pts',(13.5713223399655,0.141023010189178,3.42398486344345));
#23113=CARTESIAN_POINT('Ctrl Pts',(13.5949364561154,0.39753334322815,3.55994526707815));
#23114=CARTESIAN_POINT('Ctrl Pts',(13.6185505722652,0.55877204319843,3.8013678508274));
#23115=CARTESIAN_POINT('Ctrl Pts',(13.6421646884151,0.586097133215014,4.09039401187145));
#23116=CARTESIAN_POINT('Ctrl Pts',(13.665778804565,0.47295996523623,4.35775661870721));
#23117=CARTESIAN_POINT('Ctrl Pts',(13.6893929207148,0.24647464915429,4.53938036140496));
#23118=CARTESIAN_POINT('Ctrl Pts',(13.7130070368647,-0.0390800323908759,
4.59173784568287));
#23119=CARTESIAN_POINT('Ctrl Pts',(13.7366211530146,-0.315268912124245,
4.50228123595558));
#23120=CARTESIAN_POINT('Ctrl Pts',(13.7602352691644,-0.515901402373503,
4.29244943148197));
#23121=CARTESIAN_POINT('Ctrl Pts',(13.7838493853143,-0.59289453017979,4.01253008491428));
#23122=CARTESIAN_POINT('Ctrl Pts',(13.8074635014642,-0.527796356489121,
3.72960781627073));
#23123=CARTESIAN_POINT('Ctrl Pts',(13.831077617614,-0.336208111796874,3.51148691674935));
#23124=CARTESIAN_POINT('Ctrl Pts',(13.8546917337639,-0.0640452526541193,
3.4104415783338));
#23125=CARTESIAN_POINT('Ctrl Pts',(13.8783058499138,0.223466497127862,3.45068801978614));
#23126=CARTESIAN_POINT('Ctrl Pts',(13.9019199660636,0.457422945247278,3.62258090124322));
#23127=CARTESIAN_POINT('Ctrl Pts',(13.9255340822135,0.581754800262342,3.88492489705937));
#23128=CARTESIAN_POINT('Ctrl Pts',(13.9491481983634,0.566665067602596,4.17484744237197));
#23129=CARTESIAN_POINT('Ctrl Pts',(13.9727623145132,0.415770106744681,4.42286658094793));
#23130=CARTESIAN_POINT('Ctrl Pts',(13.9963764306631,0.165232945489059,4.56954279968241));
#23131=CARTESIAN_POINT('Ctrl Pts',(14.019990546813,-0.124903441395439,4.57972412169294));
#23132=CARTESIAN_POINT('Ctrl Pts',(14.0436046629628,-0.385105849054417,
4.45097052228405));
#23133=CARTESIAN_POINT('Ctrl Pts',(14.0672187791127,-0.553014959135429,
4.21413869785145));
#23134=CARTESIAN_POINT('Ctrl Pts',(14.0908328952626,-0.58839018453545,3.92598704378684));
#23135=CARTESIAN_POINT('Ctrl Pts',(14.1144470114124,-0.482753606228458,
3.65557310990793));
#23136=CARTESIAN_POINT('Ctrl Pts',(14.1380611275623,-0.261421765577673,
3.46770347791168));
#23137=CARTESIAN_POINT('Ctrl Pts',(14.1616752437122,0.0225616210391343,
3.40740241293002));
#23138=CARTESIAN_POINT('Ctrl Pts',(14.185289359862,0.301137958114838,3.48912148496193));
#23139=CARTESIAN_POINT('Ctrl Pts',(14.2089034760119,0.507544487205137,3.69327614952086));
#23140=CARTESIAN_POINT('Ctrl Pts',(14.2325175921618,0.592314446747875,3.97093932005559));
#23141=CARTESIAN_POINT('Ctrl Pts',(14.2561317083116,0.535132125826274,4.25556708484021));
#23142=CARTESIAN_POINT('Ctrl Pts',(14.2797458244615,0.349701665714674,4.47894641865396));
#23143=CARTESIAN_POINT('Ctrl Pts',(14.3033599406114,0.0804627670229728,
4.58754290912926));
#23144=CARTESIAN_POINT('Ctrl Pts',(14.3269740567612,-0.208059593914322,
4.55533065134682));
#23145=CARTESIAN_POINT('Ctrl Pts',(14.3505881729111,-0.44671902479684,4.39002953712461));
#23146=CARTESIAN_POINT('Ctrl Pts',(14.374202289061,-0.578319131624566,4.13125512920294));
#23147=CARTESIAN_POINT('Ctrl Pts',(14.3978164052108,-0.571321032683373,
3.84102451585645));
#23148=CARTESIAN_POINT('Ctrl Pts',(14.4214305213607,-0.427401871100662,
3.58889348396707));
#23149=CARTESIAN_POINT('Ctrl Pts',(14.4450446375106,-0.181052875819672,
3.43528699049651));
#23150=CARTESIAN_POINT('Ctrl Pts',(14.4686587536604,0.108686701521778,3.41701790091169));
#23151=CARTESIAN_POINT('Ctrl Pts',(14.4922728698103,0.372378754238714,3.53846452970905));
#23152=CARTESIAN_POINT('Ctrl Pts',(14.5158869859602,0.546827646247725,3.77052134686598));
#23153=CARTESIAN_POINT('Ctrl Pts',(14.53950110211,0.59022548618159,4.05757432072539));
#23154=CARTESIAN_POINT('Ctrl Pts',(14.5631152182599,0.492171679592087,4.3308292078278));
#23155=CARTESIAN_POINT('Ctrl Pts',(14.5867293344098,0.276165503816305,4.52479857226205));
#23156=CARTESIAN_POINT('Ctrl Pts',(14.6103434505596,-0.00602565743375084,
4.59299630554951));
#23157=CARTESIAN_POINT('Ctrl Pts',(14.6339575667095,-0.286772727926288,
4.51907834617235));
#23158=CARTESIAN_POINT('Ctrl Pts',(14.6575716828594,-0.49879271786407,4.32075964763751));
#23159=CARTESIAN_POINT('Ctrl Pts',(14.6811857990092,-0.591273560669336,
4.04556866666751));
#23160=CARTESIAN_POINT('Ctrl Pts',(14.7047999151591,-0.542051578672567,
3.75945683743125));
#23161=CARTESIAN_POINT('Ctrl Pts',(14.728414031309,-0.362923162297683,3.53099285177933));
#23162=CARTESIAN_POINT('Ctrl Pts',(14.7520281474588,-0.0968176839575538,
3.41492969374656));
#23163=CARTESIAN_POINT('Ctrl Pts',(14.7756422636087,0.192490826988301,3.43908270827084));
#23164=CARTESIAN_POINT('Ctrl Pts',(14.7992563797586,0.435667569828913,3.59766345479839));
#23165=CARTESIAN_POINT('Ctrl Pts',(14.8228704959084,0.574433549780463,3.85266695881428));
#23166=CARTESIAN_POINT('Ctrl Pts',(14.8464846120583,0.575532524168,4.14297984400973));
#23167=CARTESIAN_POINT('Ctrl Pts',(14.8700987282082,0.438701136655627,4.39902663091346));
#23168=CARTESIAN_POINT('Ctrl Pts',(14.893712844358,0.196731937819222,4.55944387228049));
#23169=CARTESIAN_POINT('Ctrl Pts',(14.9173269605079,-0.0923853752310475,
4.58578657160514));
#23170=CARTESIAN_POINT('Ctrl Pts',(14.9409410766578,-0.359362027571537,
4.47174127747511));
#23171=CARTESIAN_POINT('Ctrl Pts',(14.9645551928076,-0.540214773976066,
4.24464025294543));
#23172=CARTESIAN_POINT('Ctrl Pts',(14.9881693089575,-0.59160192159185,3.95890873763601));
#23173=CARTESIAN_POINT('Ctrl Pts',(15.0117834251074,-0.501206205285789,
3.68302663884805));
#23174=CARTESIAN_POINT('Ctrl Pts',(15.0353975412572,-0.290695865081771,
3.48310596742652));
#23175=CARTESIAN_POINT('Ctrl Pts',(15.0590116574071,-0.0105122258222001,
3.40706994202017));
#23176=CARTESIAN_POINT('Ctrl Pts',(15.082625773557,0.272176412698783,3.47311795657709));
#23177=CARTESIAN_POINT('Ctrl Pts',(15.1062398897068,0.489659512974156,3.66547122397039));
#23178=CARTESIAN_POINT('Ctrl Pts',(15.1219826338067,0.5563490739778,3.84710486709154));
#23179=CARTESIAN_POINT('Ctrl Pts',(15.1298540058567,0.566167676482186,3.94044192881839));
#23180=CARTESIAN_POINT('Ctrl Pts',(12.4701459941433,0.254789069842909,4.44592641788345));
#23181=CARTESIAN_POINT('Ctrl Pts',(12.4780173661933,0.181274697121691,4.48793034026739));
#23182=CARTESIAN_POINT('Ctrl Pts',(12.4937601102932,0.0131377437512366,
4.53483083224977));
#23183=CARTESIAN_POINT('Ctrl Pts',(12.517374226443,-0.242323003376296,4.47697306011837));
#23184=CARTESIAN_POINT('Ctrl Pts',(12.5409883425929,-0.439671888977142,
4.30480445207012));
#23185=CARTESIAN_POINT('Ctrl Pts',(12.5646024587428,-0.531669448515955,
4.05958515863483));
#23186=CARTESIAN_POINT('Ctrl Pts',(12.5882165748926,-0.496240142441994,
3.80008637217214));
#23187=CARTESIAN_POINT('Ctrl Pts',(12.6118306910425,-0.341887499674706,
3.58849794711368));
#23188=CARTESIAN_POINT('Ctrl Pts',(12.6354448071924,-0.105597250297878,
3.47552899021694));
#23189=CARTESIAN_POINT('Ctrl Pts',(12.6590589233422,0.155999231932725,3.4882530946792));
#23190=CARTESIAN_POINT('Ctrl Pts',(12.6826730394921,0.380209824197002,3.62362093815591));
#23191=CARTESIAN_POINT('Ctrl Pts',(12.706287155642,0.513300292941022,3.84919062944795));
#23192=CARTESIAN_POINT('Ctrl Pts',(12.7299012717918,0.52337486302099,4.11090284295443));
#23193=CARTESIAN_POINT('Ctrl Pts',(12.7535153879417,0.408018961865605,4.34603641497018));
#23194=CARTESIAN_POINT('Ctrl Pts',(12.7771295040916,0.194878495711741,4.49823995272895));
#23195=CARTESIAN_POINT('Ctrl Pts',(12.8007436202414,-0.0649659676909401,
4.53103681671432));
#23196=CARTESIAN_POINT('Ctrl Pts',(12.8243577363913,-0.30924088042124,4.43656701116699));
#23197=CARTESIAN_POINT('Ctrl Pts',(12.8479718525412,-0.479404065419363,
4.23747088215356));
#23198=CARTESIAN_POINT('Ctrl Pts',(12.871585968691,-0.534674727916345,3.9814632031866));
#23199=CARTESIAN_POINT('Ctrl Pts',(12.8952000848409,-0.461806870250484,
3.72989799658434));
#23200=CARTESIAN_POINT('Ctrl Pts',(12.9188142009908,-0.278263781132688,
3.54306461538724));
#23201=CARTESIAN_POINT('Ctrl Pts',(12.9424283171406,-0.0280328398727138,
3.46573897998727));
#23202=CARTESIAN_POINT('Ctrl Pts',(12.9660424332905,0.228916366652986,3.51645271720832));
#23203=CARTESIAN_POINT('Ctrl Pts',(12.9896565494404,0.431004172325429,3.68305192688505));
#23204=CARTESIAN_POINT('Ctrl Pts',(13.0132706655902,0.529798827743877,3.92560994866724));
#23205=CARTESIAN_POINT('Ctrl Pts',(13.0368847817401,0.501623505980173,4.1859960641053));
#23206=CARTESIAN_POINT('Ctrl Pts',(13.06049889789,0.353230619039521,4.40180692799916));
#23207=CARTESIAN_POINT('Ctrl Pts',(13.0841130140398,0.120183555287252,4.52132196448402));
#23208=CARTESIAN_POINT('Ctrl Pts',(13.1077271301897,-0.14166633412753,4.51589856308179));
#23209=CARTESIAN_POINT('Ctrl Pts',(13.1313412463396,-0.369564900381594,
4.38683647969259));
#23210=CARTESIAN_POINT('Ctrl Pts',(13.1549553624894,-0.508894665592834,
4.16506634104549));
#23211=CARTESIAN_POINT('Ctrl Pts',(13.1785694786393,-0.5262642816069,3.9037369046842));
#23212=CARTESIAN_POINT('Ctrl Pts',(13.2021835947892,-0.417510999030181,
3.66547758923531));
#23213=CARTESIAN_POINT('Ctrl Pts',(13.225797710939,-0.208698299100604,3.50738889824983));
#23214=CARTESIAN_POINT('Ctrl Pts',(13.2494118270889,0.0501304010278875,
3.46735788703128));
#23215=CARTESIAN_POINT('Ctrl Pts',(13.2730259432388,0.296945001575366,3.55497826608759));
#23216=CARTESIAN_POINT('Ctrl Pts',(13.2966400593886,0.472594665360713,3.74925120162283));
#23217=CARTESIAN_POINT('Ctrl Pts',(13.3202541755385,0.534983727701048,4.00361783223636));
#23218=CARTESIAN_POINT('Ctrl Pts',(13.3438682916884,0.469160215495142,4.25711742416948));
#23219=CARTESIAN_POINT('Ctrl Pts',(13.3674824078382,0.290899191662876,4.44899703551904));
#23220=CARTESIAN_POINT('Ctrl Pts',(13.3910965239881,0.0429221515009326,
4.53327138168622));
#23221=CARTESIAN_POINT('Ctrl Pts',(13.414710640138,-0.215341481063824,4.48974352894983));
#23222=CARTESIAN_POINT('Ctrl Pts',(13.4383247562878,-0.421997028626747,
4.32884523023027));
#23223=CARTESIAN_POINT('Ctrl Pts',(13.4619388724377,-0.527518050615216,
4.08913688288313));
#23224=CARTESIAN_POINT('Ctrl Pts',(13.4855529885876,-0.506615699542168,
3.82806626104107));
#23225=CARTESIAN_POINT('Ctrl Pts',(13.5091671047374,-0.364299369350597,
3.60820075662942));
#23226=CARTESIAN_POINT('Ctrl Pts',(13.5327812208873,-0.134676159283021,
3.48223266833859));
#23227=CARTESIAN_POINT('Ctrl Pts',(13.5563953370372,0.127223129883027,3.48035112543394));
#23228=CARTESIAN_POINT('Ctrl Pts',(13.580009453187,0.35863251032937,3.60300705277064));
#23229=CARTESIAN_POINT('Ctrl Pts',(13.6036235693369,0.504093113113068,3.82080510351303));
#23230=CARTESIAN_POINT('Ctrl Pts',(13.6272376854868,0.528744292176554,4.08154845863482));
#23231=CARTESIAN_POINT('Ctrl Pts',(13.6508518016366,0.426678220852065,4.32274815795836));
#23232=CARTESIAN_POINT('Ctrl Pts',(13.6744659177865,0.222355743648963,4.48659901446809));
#23233=CARTESIAN_POINT('Ctrl Pts',(13.6980800339364,-0.0352558354131549,
4.53383302978021));
#23234=CARTESIAN_POINT('Ctrl Pts',(13.7216941500862,-0.284418108090716,
4.45313024331322));
#23235=CARTESIAN_POINT('Ctrl Pts',(13.7453082662361,-0.465417601233682,
4.26383163964332));
#23236=CARTESIAN_POINT('Ctrl Pts',(13.768922382386,-0.534876526311652,4.01130394691162));
#23237=CARTESIAN_POINT('Ctrl Pts',(13.7925364985358,-0.476148568402614,
3.75606718461195));
#23238=CARTESIAN_POINT('Ctrl Pts',(13.8161506146857,-0.303308291444651,
3.55929061961886));
#23239=CARTESIAN_POINT('Ctrl Pts',(13.8397647308356,-0.0577780710103693,
3.46813312556118));
#23240=CARTESIAN_POINT('Ctrl Pts',(13.8633788469854,0.201599066354243,3.50444123046797));
#23241=CARTESIAN_POINT('Ctrl Pts',(13.8869929631353,0.412661584067771,3.65951344424533));
#23242=CARTESIAN_POINT('Ctrl Pts',(13.9106070792852,0.52482688048259,3.89618563135138));
#23243=CARTESIAN_POINT('Ctrl Pts',(13.934221195435,0.511213761492322,4.157737654591));
#23244=CARTESIAN_POINT('Ctrl Pts',(13.9578353115849,0.375084705828511,4.38148675084272));
#23245=CARTESIAN_POINT('Ctrl Pts',(13.9814494277348,0.149063989321389,4.51380989159668));
#23246=CARTESIAN_POINT('Ctrl Pts',(14.0050635438846,-0.112680949911453,
4.52299491502504));
#23247=CARTESIAN_POINT('Ctrl Pts',(14.0286776600345,-0.347421115087809,
4.40684056632315));
#23248=CARTESIAN_POINT('Ctrl Pts',(14.0522917761844,-0.498899391517477,
4.19318404374712));
#23249=CARTESIAN_POINT('Ctrl Pts',(14.0759058923342,-0.530812955762567,
3.93322962026762));
#23250=CARTESIAN_POINT('Ctrl Pts',(14.0995200084841,-0.435513499990629,
3.68927718310219));
#23251=CARTESIAN_POINT('Ctrl Pts',(14.123134124634,-0.235840202189154,3.51979163205294));
#23252=CARTESIAN_POINT('Ctrl Pts',(14.1467482407838,0.020353841830372,3.46539135927508));
#23253=CARTESIAN_POINT('Ctrl Pts',(14.1703623569337,0.271669945965271,3.53911376883853));
#23254=CARTESIAN_POINT('Ctrl Pts',(14.1939764730836,0.457878456363209,3.72329077208477));
#23255=CARTESIAN_POINT('Ctrl Pts',(14.2175905892334,0.534353207246894,3.97378306806742));
#23256=CARTESIAN_POINT('Ctrl Pts',(14.2412047053833,0.482766492200443,4.23055843429265));
#23257=CARTESIAN_POINT('Ctrl Pts',(14.2648188215332,0.315481426597312,4.4320788667444));
#23258=CARTESIAN_POINT('Ctrl Pts',(14.288432937683,0.0725890409372144,4.53004859093371));
#23259=CARTESIAN_POINT('Ctrl Pts',(14.3120470538329,-0.187699813700353,
4.50098848045824));
#23260=CARTESIAN_POINT('Ctrl Pts',(14.3356611699828,-0.40300510134274,4.35186299309067));
#23261=CARTESIAN_POINT('Ctrl Pts',(14.3592752861326,-0.521727410993515,
4.11841108999162));
#23262=CARTESIAN_POINT('Ctrl Pts',(14.3828894022825,-0.515414114678713,
3.85658114487643));
#23263=CARTESIAN_POINT('Ctrl Pts',(14.4065035184324,-0.385578237809175,
3.62912252677875));
#23264=CARTESIAN_POINT('Ctrl Pts',(14.4301176345822,-0.163335852108122,
3.49054727694211));
#23265=CARTESIAN_POINT('Ctrl Pts',(14.4537317507321,0.0980511075867261,
3.47406591865897));
#23266=CARTESIAN_POINT('Ctrl Pts',(14.477345866882,0.335939436781555,3.58362832417432));
#23267=CARTESIAN_POINT('Ctrl Pts',(14.5009599830318,0.493317541363497,3.79297710030521));
#23268=CARTESIAN_POINT('Ctrl Pts',(14.5245740991817,0.532468663007706,4.05194035550473));
#23269=CARTESIAN_POINT('Ctrl Pts',(14.5481882153316,0.444009962867018,4.2984557429324));
#23270=CARTESIAN_POINT('Ctrl Pts',(14.5718023314814,0.249141184223067,4.47344413391656));
#23271=CARTESIAN_POINT('Ctrl Pts',(14.5954164476313,-0.00543601357889273,
4.53496834239941));
#23272=CARTESIAN_POINT('Ctrl Pts',(14.6190305637812,-0.258710432878536,
4.46828366353805));
#23273=CARTESIAN_POINT('Ctrl Pts',(14.642644679931,-0.449983095981302,4.28937154481299));
#23274=CARTESIAN_POINT('Ctrl Pts',(14.6662587960809,-0.533414177619135,
4.0411095209942));
#23275=CARTESIAN_POINT('Ctrl Pts',(14.6898729122308,-0.489008838375032,
3.78299531421925));
#23276=CARTESIAN_POINT('Ctrl Pts',(14.7134870283806,-0.327409126727749,
3.57688779119022));
#23277=CARTESIAN_POINT('Ctrl Pts',(14.7371011445305,-0.0873435389344073,
3.47218205409647));
#23278=CARTESIAN_POINT('Ctrl Pts',(14.7607152606804,0.173654536592096,3.49397156277145));
#23279=CARTESIAN_POINT('Ctrl Pts',(14.7843293768302,0.393035092271916,3.63703430753458));
#23280=CARTESIAN_POINT('Ctrl Pts',(14.8079434929801,0.518222054789869,3.86708431049878));
#23281=CARTESIAN_POINT('Ctrl Pts',(14.8315576091299,0.519213488464815,4.12898847670818));
#23282=CARTESIAN_POINT('Ctrl Pts',(14.8551717252798,0.395771807832633,4.35997967156842));
#23283=CARTESIAN_POINT('Ctrl Pts',(14.8787858414297,0.177480631307892,4.50469920000947));
#23284=CARTESIAN_POINT('Ctrl Pts',(14.9023999575796,-0.0833449560929437,
4.52846412073519));
#23285=CARTESIAN_POINT('Ctrl Pts',(14.9260140737294,-0.324196468699902,
4.42557878841823));
#23286=CARTESIAN_POINT('Ctrl Pts',(14.9496281898793,-0.487351775161311,
4.22070085323907));
#23287=CARTESIAN_POINT('Ctrl Pts',(14.9732423060292,-0.533710406612102,
3.96292974457304));
#23288=CARTESIAN_POINT('Ctrl Pts',(14.996856422179,-0.452160410331013,3.71404423263127));
#23289=CARTESIAN_POINT('Ctrl Pts',(15.0204705383289,-0.262249669398955,
3.53368690291293));
#23290=CARTESIAN_POINT('Ctrl Pts',(15.0440846544788,-0.0094835464747447,
3.46509142247974));
#23291=CARTESIAN_POINT('Ctrl Pts',(15.0676987706286,0.245542447700007,3.52467627408104));
#23292=CARTESIAN_POINT('Ctrl Pts',(15.0913128867785,0.441743625625371,3.69820671204414));
#23293=CARTESIAN_POINT('Ctrl Pts',(15.1070556308784,0.501907244810829,3.86206650016617));
#23294=CARTESIAN_POINT('Ctrl Pts',(15.1149270029284,0.510765042839744,3.94627001497588));
#23295=CARTESIAN_POINT('Ctrl Pts',(12.4552189912149,0.227152124655503,4.39755682347243));
#23296=CARTESIAN_POINT('Ctrl Pts',(12.4630903632649,0.161611848667067,4.43500458455284));
#23297=CARTESIAN_POINT('Ctrl Pts',(12.4788331073648,0.0117126939868845,
4.476817784812));
#23298=CARTESIAN_POINT('Ctrl Pts',(12.5024472235147,-0.216038251184659,
4.42523583949706));
#23299=CARTESIAN_POINT('Ctrl Pts',(12.5260613396645,-0.391980722697534,
4.27174234332294));
#23300=CARTESIAN_POINT('Ctrl Pts',(12.5496754558144,-0.473999316058885,
4.05312196237532));
#23301=CARTESIAN_POINT('Ctrl Pts',(12.5732895719643,-0.442413023308054,
3.82177098359562));
#23302=CARTESIAN_POINT('Ctrl Pts',(12.5969036881141,-0.304802996424253,
3.6331335340607));
#23303=CARTESIAN_POINT('Ctrl Pts',(12.620517804264,-0.0941431270098475,
3.53241830873714));
#23304=CARTESIAN_POINT('Ctrl Pts',(12.6441319204139,0.139078010685439,3.54376223084778));
#23305=CARTESIAN_POINT('Ctrl Pts',(12.6677460365637,0.338968502198674,3.66444673774097));
#23306=CARTESIAN_POINT('Ctrl Pts',(12.6913601527136,0.457622660971028,3.86554890694496));
#23307=CARTESIAN_POINT('Ctrl Pts',(12.7149742688635,0.46660444343158,4.09887322255608));
#23308=CARTESIAN_POINT('Ctrl Pts',(12.7385883850133,0.36376118545685,4.30850187928827));
#23309=CARTESIAN_POINT('Ctrl Pts',(12.7622025011632,0.173740044570527,4.44419591437112));
#23310=CARTESIAN_POINT('Ctrl Pts',(12.7858166173131,-0.0579191156056905,
4.47343530576616));
#23311=CARTESIAN_POINT('Ctrl Pts',(12.809430733463,-0.275697552729921,4.38921263067613));
#23312=CARTESIAN_POINT('Ctrl Pts',(12.8330448496128,-0.42740315389367,4.2117124390707));
#23313=CARTESIAN_POINT('Ctrl Pts',(12.8566589657627,-0.476678613100171,
3.98347388770222));
#23314=CARTESIAN_POINT('Ctrl Pts',(12.8802730819125,-0.411714724743029,
3.75919593416074));
#23315=CARTESIAN_POINT('Ctrl Pts',(12.9038871980624,-0.248080536335154,
3.59262835132974));
#23316=CARTESIAN_POINT('Ctrl Pts',(12.9275013142123,-0.0249921205063485,
3.52369021994808));
#23317=CARTESIAN_POINT('Ctrl Pts',(12.9511154303621,0.204085831019768,3.5689030431123));
#23318=CARTESIAN_POINT('Ctrl Pts',(12.974729546512,0.384253192413122,3.71743125300502));
#23319=CARTESIAN_POINT('Ctrl Pts',(12.9983436626619,0.472331601336806,3.93367903017235));
#23320=CARTESIAN_POINT('Ctrl Pts',(13.0219577788117,0.44721245393608,4.16582108944128));
#23321=CARTESIAN_POINT('Ctrl Pts',(13.0455718949616,0.314915728754283,4.35822297028905));
#23322=CARTESIAN_POINT('Ctrl Pts',(13.0691860111115,0.107147256940744,4.46477422259573));
#23323=CARTESIAN_POINT('Ctrl Pts',(13.0928001272613,-0.126299800886535,
4.4599390970068));
#23324=CARTESIAN_POINT('Ctrl Pts',(13.1164142434112,-0.329478232215912,
4.34487636502855));
#23325=CARTESIAN_POINT('Ctrl Pts',(13.1400283595611,-0.453694911585238,
4.14716161137019));
#23326=CARTESIAN_POINT('Ctrl Pts',(13.1636424757109,-0.469180447069464,
3.9141785531052));
#23327=CARTESIAN_POINT('Ctrl Pts',(13.1872565918608,-0.372223622289685,
3.70176320202068));
#23328=CARTESIAN_POINT('Ctrl Pts',(13.2108707080107,-0.186060815253654,
3.56082237569912));
#23329=CARTESIAN_POINT('Ctrl Pts',(13.2344848241605,0.0446927613901878,
3.52513352430527));
#23330=CARTESIAN_POINT('Ctrl Pts',(13.2580989403104,0.26473540664544,3.60324972951781));
#23331=CARTESIAN_POINT('Ctrl Pts',(13.2817130564603,0.421332368785403,3.77644989896424));
#23332=CARTESIAN_POINT('Ctrl Pts',(13.3053271726101,0.476954095708811,4.00322540633176));
#23333=CARTESIAN_POINT('Ctrl Pts',(13.32894128876,0.418270453356816,4.22922792261873));
#23334=CARTESIAN_POINT('Ctrl Pts',(13.3525554049099,0.259345385135757,4.40029437151701));
#23335=CARTESIAN_POINT('Ctrl Pts',(13.3761695210597,0.0382663899759653,
4.47542748769673));
#23336=CARTESIAN_POINT('Ctrl Pts',(13.3997836372096,-0.19198341192685,4.43662109683837));
#23337=CARTESIAN_POINT('Ctrl Pts',(13.4233977533595,-0.376223052699929,
4.29317542065556));
#23338=CARTESIAN_POINT('Ctrl Pts',(13.4470118695093,-0.470298219877544,
4.07946821401937));
#23339=CARTESIAN_POINT('Ctrl Pts',(13.4706259856592,-0.451663144756522,
3.84671589668833));
#23340=CARTESIAN_POINT('Ctrl Pts',(13.4942401018091,-0.324783852814677,
3.65069918177841));
#23341=CARTESIAN_POINT('Ctrl Pts',(13.5178542179589,-0.120067849615538,
3.53839483955645));
#23342=CARTESIAN_POINT('Ctrl Pts',(13.5414683341088,0.113423249576877,3.53671738742444));
#23343=CARTESIAN_POINT('Ctrl Pts',(13.5650824502587,0.319731677430589,3.64606883846313));
#23344=CARTESIAN_POINT('Ctrl Pts',(13.5886965664085,0.449414183027706,3.84024235619866));
#23345=CARTESIAN_POINT('Ctrl Pts',(13.6123106825584,0.471391451138094,4.07270290539818));
#23346=CARTESIAN_POINT('Ctrl Pts',(13.6359247987083,0.380396476467901,4.28773969720951));
#23347=CARTESIAN_POINT('Ctrl Pts',(13.6595389148581,0.198236838143636,4.43381766753122));
#23348=CARTESIAN_POINT('Ctrl Pts',(13.683153031008,-0.0314316384354341,
4.47592821387755));
#23349=CARTESIAN_POINT('Ctrl Pts',(13.7067671471579,-0.253567304057185,
4.40397925067086));
#23350=CARTESIAN_POINT('Ctrl Pts',(13.7303812633077,-0.414933800093862,
4.23521384780468));
#23351=CARTESIAN_POINT('Ctrl Pts',(13.7539953794576,-0.476858522443512,
4.01007780890896));
#23352=CARTESIAN_POINT('Ctrl Pts',(13.7776094956075,-0.424500780316106,
3.78252655295316));
#23353=CARTESIAN_POINT('Ctrl Pts',(13.8012236117573,-0.270408471092428,
3.60709432248837));
#23354=CARTESIAN_POINT('Ctrl Pts',(13.8248377279072,-0.0515108893666192,
3.52582467278856));
#23355=CARTESIAN_POINT('Ctrl Pts',(13.8484518440571,0.179731635580624,3.55819444114981));
#23356=CARTESIAN_POINT('Ctrl Pts',(13.8720659602069,0.367900222888263,3.69644598724744));
#23357=CARTESIAN_POINT('Ctrl Pts',(13.8956800763568,0.467898960702838,3.90744636564338));
#23358=CARTESIAN_POINT('Ctrl Pts',(13.9192941925067,0.455762455382048,4.14062786681004));
#23359=CARTESIAN_POINT('Ctrl Pts',(13.9429083086565,0.33439930491234,4.34010692073752));
#23360=CARTESIAN_POINT('Ctrl Pts',(13.9665224248064,0.132895033153719,4.45807698351094));
#23361=CARTESIAN_POINT('Ctrl Pts',(13.9901365409563,-0.100458458427467,
4.46626570835715));
#23362=CARTESIAN_POINT('Ctrl Pts',(14.0137506571061,-0.309736381121202,
4.36271061036225));
#23363=CARTESIAN_POINT('Ctrl Pts',(14.037364773256,-0.444783823899526,4.1722293896428));
#23364=CARTESIAN_POINT('Ctrl Pts',(14.0609788894059,-0.473235726989685,
3.94047219674841));
#23365=CARTESIAN_POINT('Ctrl Pts',(14.0845930055557,-0.388273393752801,
3.72298125629644));
#23366=CARTESIAN_POINT('Ctrl Pts',(14.1082071217056,-0.210258638800633,
3.5718797861942));
#23367=CARTESIAN_POINT('Ctrl Pts',(14.1318212378555,0.0181460626216094,
3.52338030562014));
#23368=CARTESIAN_POINT('Ctrl Pts',(14.1554353540053,0.242201933815703,3.58910605271512));
#23369=CARTESIAN_POINT('Ctrl Pts',(14.1790494701552,0.40821242552128,3.75330539464867));
#23370=CARTESIAN_POINT('Ctrl Pts',(14.2026635863051,0.476391967745912,3.97662681607925));
#23371=CARTESIAN_POINT('Ctrl Pts',(14.2262777024549,0.430400858574612,4.20554978374509));
#23372=CARTESIAN_POINT('Ctrl Pts',(14.2498918186048,0.28126118747995,4.38521131483484));
#23373=CARTESIAN_POINT('Ctrl Pts',(14.2735059347547,0.0647153148514563,
4.47255427273816));
#23374=CARTESIAN_POINT('Ctrl Pts',(14.2971200509045,-0.167340033486385,
4.44664630956965));
#23375=CARTESIAN_POINT('Ctrl Pts',(14.3207341670544,-0.359291177888639,
4.31369644905674));
#23376=CARTESIAN_POINT('Ctrl Pts',(14.3443482832043,-0.465135690362464,
4.10556705078029));
#23377=CARTESIAN_POINT('Ctrl Pts',(14.3679623993541,-0.459507196674052,
3.87213777389641));
#23378=CARTESIAN_POINT('Ctrl Pts',(14.391576515504,-0.343754604517688,3.66935156959044));
#23379=CARTESIAN_POINT('Ctrl Pts',(14.4151906316539,-0.145618828396573,
3.5458075633877));
#23380=CARTESIAN_POINT('Ctrl Pts',(14.4388047478037,0.0874155136516737,
3.53111393640625));
#23381=CARTESIAN_POINT('Ctrl Pts',(14.4624188639536,0.299500119324396,3.6287921186396));
#23382=CARTESIAN_POINT('Ctrl Pts',(14.4860329801035,0.439807436479269,3.81543285374444));
#23383=CARTESIAN_POINT('Ctrl Pts',(14.5096470962533,0.474711839833821,4.04630639028407));
#23384=CARTESIAN_POINT('Ctrl Pts',(14.5332612124032,0.395848246141948,4.26608227803701));
#23385=CARTESIAN_POINT('Ctrl Pts',(14.5568753285531,0.22211686462983,4.42208969557108));
#23386=CARTESIAN_POINT('Ctrl Pts',(14.5804894447029,-0.00484636972403486,
4.47694037924932));
#23387=CARTESIAN_POINT('Ctrl Pts',(14.6041035608528,-0.230648137830783,
4.41748898090375));
#23388=CARTESIAN_POINT('Ctrl Pts',(14.6277176770027,-0.401173474098533,
4.25798344198848));
#23389=CARTESIAN_POINT('Ctrl Pts',(14.6513317931525,-0.475554794568933,
4.03665037532088));
#23390=CARTESIAN_POINT('Ctrl Pts',(14.6749459093024,-0.435966098077497,
3.80653379100725));
#23391=CARTESIAN_POINT('Ctrl Pts',(14.6985600254523,-0.291895091157815,
3.62278273060111));
#23392=CARTESIAN_POINT('Ctrl Pts',(14.7221741416021,-0.077869393911261,
3.52943441444639));
#23393=CARTESIAN_POINT('Ctrl Pts',(14.745788257752,0.15481824619589,3.54886041727207));
#23394=CARTESIAN_POINT('Ctrl Pts',(14.7694023739019,0.350402614714918,3.67640516027076));
#23395=CARTESIAN_POINT('Ctrl Pts',(14.7930164900517,0.462010559799276,3.88150166218328));
#23396=CARTESIAN_POINT('Ctrl Pts',(14.8166306062016,0.46289445276163,4.11499710940664));
#23397=CARTESIAN_POINT('Ctrl Pts',(14.8402447223515,0.352842479009638,4.32093271222338));
#23398=CARTESIAN_POINT('Ctrl Pts',(14.8638588385013,0.158229324796562,4.44995452773844));
#23399=CARTESIAN_POINT('Ctrl Pts',(14.8874729546512,-0.07430453695484,4.47114166986524));
#23400=CARTESIAN_POINT('Ctrl Pts',(14.9110870708011,-0.289030909828268,
4.37941629936134));
#23401=CARTESIAN_POINT('Ctrl Pts',(14.9347011869509,-0.434488776346555,
4.1967614535327));
#23402=CARTESIAN_POINT('Ctrl Pts',(14.9583153031008,-0.475818891632353,
3.96695075151007));
#23403=CARTESIAN_POINT('Ctrl Pts',(14.9819294192507,-0.403114615376237,
3.74506182641449));
#23404=CARTESIAN_POINT('Ctrl Pts',(15.0055435354005,-0.233803473716137,
3.58426783839933));
#23405=CARTESIAN_POINT('Ctrl Pts',(15.0291576515504,-0.00845486712728951,
3.5231129029393));
#23406=CARTESIAN_POINT('Ctrl Pts',(15.0527717677003,0.218908482701231,3.57623459158499));
#23407=CARTESIAN_POINT('Ctrl Pts',(15.0763858838501,0.393827738276586,3.73094220011788));
#23408=CARTESIAN_POINT('Ctrl Pts',(15.09212862795,0.447465415643859,3.87702813324079));
#23409=CARTESIAN_POINT('Ctrl Pts',(15.1,0.455362409197302,3.95209810113337));
#23410=CARTESIAN_POINT('',(15.1,0.455362409197302,3.95209810113338));
#23411=CARTESIAN_POINT('Ctrl Pts',(15.1,0.455362409197302,3.95209810113337));
#23412=CARTESIAN_POINT('Ctrl Pts',(15.1,0.461198486074795,3.93070554260298));
#23413=CARTESIAN_POINT('Ctrl Pts',(15.1,0.46535922191849,3.9089149747703));
#23414=CARTESIAN_POINT('Ctrl Pts',(15.1,0.467933495509747,3.88694781877637));
#23415=CARTESIAN_POINT('Ctrl Pts',(15.1,0.470556099470815,3.86456824322593));
#23416=CARTESIAN_POINT('Ctrl Pts',(15.1,0.471533159003394,3.84200460508655));
#23417=CARTESIAN_POINT('Ctrl Pts',(15.1,0.470938919222204,3.8194389967166));
#23418=CARTESIAN_POINT('Ctrl Pts',(15.1,0.470570970565677,3.80546654730098));
#23419=CARTESIAN_POINT('Ctrl Pts',(15.1,0.469600118414825,3.7914923521806));
#23420=CARTESIAN_POINT('Ctrl Pts',(15.1,0.468037922355437,3.77755218535593));
#23421=CARTESIAN_POINT('Ctrl Pts',(15.1,0.467305764617198,3.77101881782393));
#23422=CARTESIAN_POINT('Ctrl Pts',(15.1,0.466444065557791,3.76449770946228));
#23423=CARTESIAN_POINT('Ctrl Pts',(15.1,0.465455885979624,3.7580011302485));
#23424=CARTESIAN_POINT('Ctrl Pts',(15.1,0.462059294618766,3.73567095330476));
#23425=CARTESIAN_POINT('Ctrl Pts',(15.1,0.45716703427379,3.71360451488159));
#23426=CARTESIAN_POINT('Ctrl Pts',(15.1,0.450855318277529,3.69195899424001));
#23427=CARTESIAN_POINT('Ctrl Pts',(15.1,0.444011336009419,3.66848810937402));
#23428=CARTESIAN_POINT('Ctrl Pts',(15.1,0.435499564516811,3.64551127788848));
#23429=CARTESIAN_POINT('Ctrl Pts',(15.1,0.425460105602329,3.62314791088594));
#23430=CARTESIAN_POINT('Ctrl Pts',(15.1,0.421555366121865,3.61444992000866));
#23431=CARTESIAN_POINT('Ctrl Pts',(15.1,0.417417266816347,3.60584160863805));
#23432=CARTESIAN_POINT('Ctrl Pts',(15.1,0.413065612826793,3.5973533346642));
#23433=CARTESIAN_POINT('Ctrl Pts',(15.1,0.400188909388694,3.57223622128044));
#23434=CARTESIAN_POINT('Ctrl Pts',(15.1,0.385429835973237,3.54813135585314));
#23435=CARTESIAN_POINT('Ctrl Pts',(15.1,0.369010648251791,3.52520488756047));
#23436=CARTESIAN_POINT('Ctrl Pts',(15.1,0.352591460530346,3.50227841926781));
#23437=CARTESIAN_POINT('Ctrl Pts',(15.1,0.334512091502091,3.48052876229398));
#23438=CARTESIAN_POINT('Ctrl Pts',(15.1,0.31493781544227,3.46010549098216));
#23439=CARTESIAN_POINT('Ctrl Pts',(14.8800042915148,-1.01702808208336E-5,
4.45785711824254));
#23440=CARTESIAN_POINT('Ctrl Pts',(14.8824938458936,-0.0238866377941533,
4.45787702641871));
#23441=CARTESIAN_POINT('Ctrl Pts',(14.8849834002724,-0.0477600743578134,
4.45604121816599));
#23442=CARTESIAN_POINT('Ctrl Pts',(14.8874729546512,-0.0713366221418418,
4.45232291776013));
#23443=CARTESIAN_POINT('Ctrl Pts',(14.8953443267012,-0.145879994579315,
4.44056654636394));
#23444=CARTESIAN_POINT('Ctrl Pts',(14.9032156987511,-0.217455452203791,
4.40999142286264));
#23445=CARTESIAN_POINT('Ctrl Pts',(14.9110870708011,-0.277486158769077,
4.36426138680722));
#23446=CARTESIAN_POINT('Ctrl Pts',(14.918958442851,-0.337516865334364,4.31853135075179));
#23447=CARTESIAN_POINT('Ctrl Pts',(14.926829814901,-0.38600282084046,4.25764640214225));
#23448=CARTESIAN_POINT('Ctrl Pts',(14.9347011869509,-0.417134151141141,
4.18890214416703));
#23449=CARTESIAN_POINT('Ctrl Pts',(14.9425725590009,-0.448265481441821,
4.12015788619182));
#23450=CARTESIAN_POINT('Ctrl Pts',(14.9504439310508,-0.462042186537087,
4.04355431885095));
#23451=CARTESIAN_POINT('Ctrl Pts',(14.9583153031008,-0.456813159708701,
3.96827104766458));
#23452=CARTESIAN_POINT('Ctrl Pts',(14.9661866751508,-0.451584132880315,
3.89298777647821));
#23453=CARTESIAN_POINT('Ctrl Pts',(14.9740580472007,-0.427349374128277,
3.81902480144635));
#23454=CARTESIAN_POINT('Ctrl Pts',(14.9819294192507,-0.387013471142241,
3.7552443159279));
#23455=CARTESIAN_POINT('Ctrl Pts',(14.9898007913006,-0.346677568156205,
3.69146383040944));
#23456=CARTESIAN_POINT('Ctrl Pts',(14.9976721633506,-0.290240520936171,
3.63786583440439));
#23457=CARTESIAN_POINT('Ctrl Pts',(15.0055435354005,-0.224463896228013,
3.60087434715852));
#23458=CARTESIAN_POINT('Ctrl Pts',(15.0134149074505,-0.158687271519854,
3.56388285991266));
#23459=CARTESIAN_POINT('Ctrl Pts',(15.0212862795004,-0.0835710693235713,
3.54349788142598));
#23460=CARTESIAN_POINT('Ctrl Pts',(15.0291576515504,-0.00811907658734153,
3.54215900695692));
#23461=CARTESIAN_POINT('Ctrl Pts',(15.0370290236004,0.067332916148885,3.54082013248786));
#23462=CARTESIAN_POINT('Ctrl Pts',(15.0449003956503,0.143120699425059,3.55852736203643));
#23463=CARTESIAN_POINT('Ctrl Pts',(15.0527717677003,0.210167800325704,3.59316557823286));
#23464=CARTESIAN_POINT('Ctrl Pts',(15.0606431397502,0.27721490122635,3.62780379442929));
#23465=CARTESIAN_POINT('Ctrl Pts',(15.0685145118002,0.335521319751467,3.67937299727358));
#23466=CARTESIAN_POINT('Ctrl Pts',(15.0763858838501,0.378083948355844,3.74167908197646));
#23467=CARTESIAN_POINT('Ctrl Pts',(15.0842572559001,0.420646576960222,3.80398516667934));
#23468=CARTESIAN_POINT('Ctrl Pts',(15.09212862795,0.447465415643859,3.87702813324079));
#23469=CARTESIAN_POINT('Ctrl Pts',(15.1,0.455362409197302,3.95209810113337));
#23470=CARTESIAN_POINT('Ctrl Pts',(12.5,0.310062960217722,4.54266560670548));
#23471=CARTESIAN_POINT('Ctrl Pts',(12.5,0.283442099593322,4.54921865641189));
#23472=CARTESIAN_POINT('Ctrl Pts',(12.5,0.256466577744696,4.55390832200786));
#23473=CARTESIAN_POINT('Ctrl Pts',(12.5,0.229324391633413,4.55669460918752));
#23474=CARTESIAN_POINT('Ctrl Pts',(12.5,0.202804350211112,4.55941702996513));
#23475=CARTESIAN_POINT('Ctrl Pts',(12.5,0.176124140498118,4.56032157710196));
#23476=CARTESIAN_POINT('Ctrl Pts',(12.5,0.149491279718871,4.55933465732487));
#23477=CARTESIAN_POINT('Ctrl Pts',(12.5,0.131604301980395,4.55867182909064));
#23478=CARTESIAN_POINT('Ctrl Pts',(12.5,0.113739373486447,4.5571550748263));
#23479=CARTESIAN_POINT('Ctrl Pts',(12.5,0.0959711573489174,4.5547553284502));
#23480=CARTESIAN_POINT('Ctrl Pts',(12.5,0.0885102514788159,4.55374767063663));
#23481=CARTESIAN_POINT('Ctrl Pts',(12.5,0.0810658284660142,4.55258395860043));
#23482=CARTESIAN_POINT('Ctrl Pts',(12.5,0.0736590895785168,4.55126509319275));
#23483=CARTESIAN_POINT('Ctrl Pts',(12.5,0.0532014046082737,4.54762233847462));
#23484=CARTESIAN_POINT('Ctrl Pts',(12.5,0.0329999615976937,4.54279338637244));
#23485=CARTESIAN_POINT('Ctrl Pts',(12.5,0.0131662989716721,4.53674486487483));
#23486=CARTESIAN_POINT('Ctrl Pts',(12.5,-0.00550403753485725,4.53105111411095));
#23487=CARTESIAN_POINT('Ctrl Pts',(12.5,-0.0238485481480196,4.52427602479051));
#23488=CARTESIAN_POINT('Ctrl Pts',(12.5,-0.0417515783368052,4.51643454453567));
#23489=CARTESIAN_POINT('Ctrl Pts',(12.5,-0.0500477299146631,4.51280085190917));
#23490=CARTESIAN_POINT('Ctrl Pts',(12.5,-0.058248775177811,4.50893813195896));
#23491=CARTESIAN_POINT('Ctrl Pts',(12.5,-0.0663415323109863,4.50484786558969));
#23492=CARTESIAN_POINT('Ctrl Pts',(12.5,-0.0727048112135971,4.50163171746301));
#23493=CARTESIAN_POINT('Ctrl Pts',(12.5,-0.0789919703630761,4.49827952355299));
#23494=CARTESIAN_POINT('Ctrl Pts',(12.5,-0.085197598682301,4.4947927546146));
#23495=CARTESIAN_POINT('Ctrl Pts',(12.5,-0.104491803581693,4.48395188067351));
#23496=CARTESIAN_POINT('Ctrl Pts',(12.5,-0.123002674071495,4.47180959856144));
#23497=CARTESIAN_POINT('Ctrl Pts',(12.5,-0.140547257611399,4.45840101528927));
#23498=CARTESIAN_POINT('Ctrl Pts',(12.5,-0.156644205929787,4.44609879839914));
#23499=CARTESIAN_POINT('Ctrl Pts',(12.5,-0.17192740174072,4.43272977950413));
#23500=CARTESIAN_POINT('Ctrl Pts',(12.5,-0.186217277007305,4.41832740439832));
#23501=CARTESIAN_POINT('Origin',(15.1,0.,4.));
#23502=CARTESIAN_POINT('',(15.1,-1.16619037896906,2.5));
#23503=CARTESIAN_POINT('',(15.1,1.16619037896906,2.5));
#23504=CARTESIAN_POINT('',(15.1,1.25,2.5));
#23505=CARTESIAN_POINT('Origin',(15.1,0.,4.));
#23506=CARTESIAN_POINT('Origin',(15.1,0.,4.));
#23507=CARTESIAN_POINT('',(15.1,2.75545529808154E-17,5.725));
#23508=CARTESIAN_POINT('Origin',(15.1,0.,5.5));
#23509=CARTESIAN_POINT('',(15.1,1.5,4.225));
#23510=CARTESIAN_POINT('Origin',(15.1,1.5,4.));
#23511=CARTESIAN_POINT('',(15.1,-1.5,4.225));
#23512=CARTESIAN_POINT('Origin',(15.1,-1.5,4.));
#23513=CARTESIAN_POINT('Origin',(14.4,-1.5,4.));
#23514=CARTESIAN_POINT('',(14.5,-1.5,4.225));
#23515=CARTESIAN_POINT('Origin',(14.5,-1.5,4.));
#23516=CARTESIAN_POINT('',(14.4,-1.5,4.225));
#23517=CARTESIAN_POINT('Origin',(14.4,1.5,4.));
#23518=CARTESIAN_POINT('',(14.5,1.5,4.225));
#23519=CARTESIAN_POINT('Origin',(14.5,1.5,4.));
#23520=CARTESIAN_POINT('',(14.4,1.5,4.225));
#23521=CARTESIAN_POINT('Origin',(14.4,0.,5.5));
#23522=CARTESIAN_POINT('',(14.5,-2.75545529808154E-17,5.725));
#23523=CARTESIAN_POINT('Origin',(14.5,0.,5.5));
#23524=CARTESIAN_POINT('',(14.4,-2.75545529808154E-17,5.725));
#23525=CARTESIAN_POINT('Origin',(14.4,2.5,2.5));
#23526=CARTESIAN_POINT('',(14.5,1.16619037896906,2.5));
#23527=CARTESIAN_POINT('',(14.5,-1.16619037896906,2.5));
#23528=CARTESIAN_POINT('',(14.5,1.25,2.5));
#23529=CARTESIAN_POINT('',(14.5,1.16619037896906,2.5));
#23530=CARTESIAN_POINT('',(14.5,-1.16619037896906,2.5));
#23531=CARTESIAN_POINT('Origin',(14.5,0.,4.));
#23532=CARTESIAN_POINT('Origin',(14.5,0.,4.));
#23533=CARTESIAN_POINT('',(14.5,-1.34711147906209E-16,5.1));
#23534=CARTESIAN_POINT('Origin',(14.5,0.,4.));
#23535=CARTESIAN_POINT('Origin',(14.5,0.,4.));
#23536=CARTESIAN_POINT('Origin',(12.5,0.,4.));
#23537=CARTESIAN_POINT('Origin',(12.5,0.,4.));
#23538=CARTESIAN_POINT('',(12.5,-1.34711147906209E-16,5.1));
#23539=CARTESIAN_POINT('',(12.5,-1.34711147906209E-16,5.1));
#23540=CARTESIAN_POINT('Origin',(12.5,0.,4.));
#23541=CARTESIAN_POINT('Origin',(12.5,0.,4.));
#33915=UNCERTAINTY_MEASURE_WITH_UNIT(LENGTH_MEASURE(0.001),#33982,
'DISTANCE_ACCURACY_VALUE',
'Maximum model space distance between geometric entities at asserted c
onnectivities');
#33929=UNCERTAINTY_MEASURE_WITH_UNIT(LENGTH_MEASURE(0.001),#33982,
'DISTANCE_ACCURACY_VALUE',
'Maximum model space distance between geometric entities at asserted c
onnectivities');
#33967=(
GEOMETRIC_REPRESENTATION_CONTEXT(3)
GLOBAL_UNCERTAINTY_ASSIGNED_CONTEXT((#33915))
GLOBAL_UNIT_ASSIGNED_CONTEXT((#33982,#33984,#33985))
REPRESENTATION_CONTEXT('','3D')
);
#33981=(
GEOMETRIC_REPRESENTATION_CONTEXT(3)
GLOBAL_UNCERTAINTY_ASSIGNED_CONTEXT((#33929))
GLOBAL_UNIT_ASSIGNED_CONTEXT((#33982,#33984,#33985))
REPRESENTATION_CONTEXT('','3D')
);
#33982=(
LENGTH_UNIT()
NAMED_UNIT(*)
SI_UNIT(.CENTI.,.METRE.)
);
#33984=(
NAMED_UNIT(*)
PLANE_ANGLE_UNIT()
SI_UNIT($,.RADIAN.)
);
#33985=(
NAMED_UNIT(*)
SI_UNIT($,.STERADIAN.)
SOLID_ANGLE_UNIT()
);
#34023=SHAPE_DEFINITION_REPRESENTATION(#34087,#34219);
#34087=PRODUCT_DEFINITION_SHAPE('',$,#34271);
#34219=SHAPE_REPRESENTATION('',(#14428),#33967);
#34233=PRODUCT_DEFINITION_CONTEXT('part definition',#34388,'design');
#34271=PRODUCT_DEFINITION('Flanged lead nut','Flanged lead nut',#34322,
#34233);
#34322=PRODUCT_DEFINITION_FORMATION('',$,#34427);
#34388=APPLICATION_CONTEXT(
'Core Data for Automotive Mechanical Design Process');
#34389=PRODUCT_CONTEXT('part definition',#34388,'mechanical');
#34427=PRODUCT('Flanged lead nut','Flanged lead nut','Flanged lead nut',
(#34389));
#34518=COLOUR_RGB('Black',0.12,0.14,0.17);
#34519=FILL_AREA_STYLE_COLOUR('',#34518);
#34520=FILL_AREA_STYLE('',(#34519));
#34521=SURFACE_STYLE_FILL_AREA(#34520);
#34522=SURFACE_SIDE_STYLE('',(#34521));
#34523=SURFACE_STYLE_USAGE(.BOTH.,#34522);
#34524=PRESENTATION_STYLE_ASSIGNMENT((#34523));
ENDSEC;
END-ISO-10303-21;
